ISO-10303-21;
HEADER;
FILE_DESCRIPTION (('STEP AP214'),
    '1' );
FILE_NAME ('End Plate.step',
    '2026-10-22T18:53:08',
    ( '' ),
    ( '' ),
    'SwSTEP 2.0',
    'SolidWorks 2025',
    '' );
FILE_SCHEMA (( 'AUTOMOTIVE_DESIGN' ));
ENDSEC;

DATA;
#6=DIRECTION ( 'NONE',  ( -0.000000000000000000, -0.000000000000000000, -1.000000000000000000 ) ) ;
#15=CIRCLE ( 'NONE', #8560, 2.000000000000000000 ) ;
#16=DIRECTION ( 'NONE',  ( 1.000000000000000000, 0.000000000000000000, 0.000000000000000000 ) ) ;
#18=ORIENTED_EDGE ( 'NONE', *, *, #10304, .F. ) ;
#22=CARTESIAN_POINT ( 'NONE',  ( 33.99999999999998579, -6.000000000000013323, 12.00000000000000000 ) ) ;
#27=CARTESIAN_POINT ( 'NONE',  ( -31.10231664966676846, 45.36128193761570770, 11.00000000000000000 ) ) ;
#38=DIRECTION ( 'NONE',  ( -0.4828336235133057208, -0.8757121056631633760, 0.000000000000000000 ) ) ;
#40=AXIS2_PLACEMENT_3D ( 'NONE', #5104, #5351, #18285 ) ;
#53=ORIENTED_EDGE ( 'NONE', *, *, #10449, .T. ) ;
#66=DIRECTION ( 'NONE',  ( 1.000000000000000000, 0.000000000000000000, -0.000000000000000000 ) ) ;
#81=AXIS2_PLACEMENT_3D ( 'NONE', #23504, #16172, #14329 ) ;
#91=ORIENTED_EDGE ( 'NONE', *, *, #20484, .F. ) ;
#95=CARTESIAN_POINT ( 'NONE',  ( 20.85000000000000497, -16.67999999999999616, 13.00000000000000178 ) ) ;
#98=AXIS2_PLACEMENT_3D ( 'NONE', #4518, #4374, #19265 ) ;
#115=CARTESIAN_POINT ( 'NONE',  ( -42.00000000000000000, -6.000000000000000888, 12.00000000000000000 ) ) ;
#117=CIRCLE ( 'NONE', #3217, 5.099999999999996980 ) ;
#118=AXIS2_PLACEMENT_3D ( 'NONE', #19032, #3780, #14981 ) ;
#119=VECTOR ( 'NONE', #13180, 1000.000000000000000 ) ;
#120=EDGE_LOOP ( 'NONE', ( #21996, #2692, #5387 ) ) ;
#121=AXIS2_PLACEMENT_3D ( 'NONE', #7421, #9361, #16 ) ;
#123=FACE_OUTER_BOUND ( 'NONE', #13538, .T. ) ;
#127=CYLINDRICAL_SURFACE ( 'NONE', #11099, 4.999999999999997335 ) ;
#137=ORIENTED_EDGE ( 'NONE', *, *, #768, .T. ) ;
#140=DIRECTION ( 'NONE',  ( -0.000000000000000000, -0.000000000000000000, -1.000000000000000000 ) ) ;
#145=VERTEX_POINT ( 'NONE', #9704 ) ;
#155=EDGE_CURVE ( 'NONE', #21886, #19378, #14378, .T. ) ;
#156=AXIS2_PLACEMENT_3D ( 'NONE', #18360, #1648, #3839 ) ;
#167=DIRECTION ( 'NONE',  ( 1.000000000000000000, 0.000000000000000000, 0.000000000000000000 ) ) ;
#171=CIRCLE ( 'NONE', #23551, 8.000000000000003553 ) ;
#176=DIRECTION ( 'NONE',  ( 1.000000000000000000, 0.000000000000000000, -0.000000000000000000 ) ) ;
#185=EDGE_LOOP ( 'NONE', ( #17761, #2920, #15803, #19074 ) ) ;
#196=AXIS2_PLACEMENT_3D ( 'NONE', #4515, #15001, #11919 ) ;
#202=CIRCLE ( 'NONE', #22024, 5.099999999999996980 ) ;
#204=ORIENTED_EDGE ( 'NONE', *, *, #22334, .T. ) ;
#209=CARTESIAN_POINT ( 'NONE',  ( 33.99999999999998579, -5.000000000000013323, 9.500000000000000000 ) ) ;
#220=DIRECTION ( 'NONE',  ( -0.000000000000000000, -1.000000000000000000, -0.000000000000000000 ) ) ;
#225=CARTESIAN_POINT ( 'NONE',  ( -21.84999999999999787, 16.67999999999985405, 13.00000000000000178 ) ) ;
#237=CARTESIAN_POINT ( 'NONE',  ( -40.00000000000000000, 28.80990663662251450, 12.00000000000000000 ) ) ;
#246=CARTESIAN_POINT ( 'NONE',  ( -40.77574956473004164, -27.49633847812775755, 0.000000000000000000 ) ) ;
#249=DIRECTION ( 'NONE',  ( 0.000000000000000000, 0.000000000000000000, -1.000000000000000000 ) ) ;
#250=LINE ( 'NONE', #18547, #2878 ) ;
#269=VECTOR ( 'NONE', #8708, 1000.000000000000000 ) ;
#273=ORIENTED_EDGE ( 'NONE', *, *, #2065, .T. ) ;
#276=ORIENTED_EDGE ( 'NONE', *, *, #7622, .T. ) ;
#280=CARTESIAN_POINT ( 'NONE',  ( 41.00000000000000000, 5.999999999999986677, 12.00000000000000000 ) ) ;
#282=VECTOR ( 'NONE', #12810, 1000.000000000000000 ) ;
#288=LINE ( 'NONE', #12948, #17547 ) ;
#291=DIRECTION ( 'NONE',  ( 0.000000000000000000, 1.000000000000000000, 0.000000000000000000 ) ) ;
#292=ORIENTED_EDGE ( 'NONE', *, *, #9808, .F. ) ;
#295=ORIENTED_EDGE ( 'NONE', *, *, #2994, .F. ) ;
#300=CARTESIAN_POINT ( 'NONE',  ( 0.000000000000000000, -45.00000000000000000, 0.000000000000000000 ) ) ;
#302=LINE ( 'NONE', #13461, #16288 ) ;
#306=DIRECTION ( 'NONE',  ( 1.000000000000000000, 0.000000000000000000, 0.000000000000000000 ) ) ;
#311=CYLINDRICAL_SURFACE ( 'NONE', #7242, 5.099999999999996980 ) ;
#320=EDGE_CURVE ( 'NONE', #7241, #1813, #6074, .T. ) ;
#324=CARTESIAN_POINT ( 'NONE',  ( -40.00000000000000000, -29.49999999999999645, 11.00000000000000000 ) ) ;
#326=CARTESIAN_POINT ( 'NONE',  ( 29.00000000000000000, 29.50000000000000355, 12.00000000000000000 ) ) ;
#338=EDGE_LOOP ( 'NONE', ( #9673, #2641, #5276, #22017 ) ) ;
#341=ORIENTED_EDGE ( 'NONE', *, *, #8197, .F. ) ;
#366=ORIENTED_EDGE ( 'NONE', *, *, #7622, .F. ) ;
#380=CARTESIAN_POINT ( 'NONE',  ( 31.10231664966676846, 45.36128193761570770, 12.00000000000000000 ) ) ;
#385=DIRECTION ( 'NONE',  ( -1.000000000000000000, 0.000000000000000000, 0.000000000000000000 ) ) ;
#399=EDGE_CURVE ( 'NONE', #3497, #3956, #12631, .T. ) ;
#411=VERTEX_POINT ( 'NONE', #10552 ) ;
#413=EDGE_LOOP ( 'NONE', ( #450, #8940, #2747, #24030 ) ) ;
#418=AXIS2_PLACEMENT_3D ( 'NONE', #13567, #8055, #21010 ) ;
#419=EDGE_LOOP ( 'NONE', ( #22193, #22078, #19514, #14610, #19694, #15843, #2106, #5083, #6149, #13689 ) ) ;
#430=VERTEX_POINT ( 'NONE', #6920 ) ;
#437=DIRECTION ( 'NONE',  ( 0.000000000000000000, -1.000000000000000000, 0.000000000000000000 ) ) ;
#443=EDGE_CURVE ( 'NONE', #14074, #21725, #10459, .T. ) ;
#446=DIRECTION ( 'NONE',  ( -0.000000000000000000, -0.000000000000000000, -1.000000000000000000 ) ) ;
#450=ORIENTED_EDGE ( 'NONE', *, *, #7005, .F. ) ;
#452=AXIS2_PLACEMENT_3D ( 'NONE', #7409, #18546, #12906 ) ;
#461=DIRECTION ( 'NONE',  ( -1.000000000000000000, -2.600433232233976523E-16, 0.000000000000000000 ) ) ;
#462=LINE ( 'NONE', #2294, #13049 ) ;
#463=DIRECTION ( 'NONE',  ( -0.000000000000000000, -0.000000000000000000, -1.000000000000000000 ) ) ;
#465=EDGE_LOOP ( 'NONE', ( #9953, #21029, #23711, #6044 ) ) ;
#466=CARTESIAN_POINT ( 'NONE',  ( 29.99999999999998934, -1.387778780781445676E-14, 9.500000000000000000 ) ) ;
#469=CIRCLE ( 'NONE', #3578, 5.999999999999998224 ) ;
#470=DIRECTION ( 'NONE',  ( -0.000000000000000000, 0.000000000000000000, 1.000000000000000000 ) ) ;
#486=CIRCLE ( 'NONE', #7856, 8.000000000000003553 ) ;
#487=VECTOR ( 'NONE', #22669, 1000.000000000000000 ) ;
#488=AXIS2_PLACEMENT_3D ( 'NONE', #7572, #19067, #22602 ) ;
#489=AXIS2_PLACEMENT_3D ( 'NONE', #4999, #8870, #14016 ) ;
#492=CIRCLE ( 'NONE', #10208, 1.000000000000001998 ) ;
#493=CIRCLE ( 'NONE', #13726, 11.00000000000001066 ) ;
#499=EDGE_LOOP ( 'NONE', ( #19745, #2721, #11674, #16253 ) ) ;
#505=DIRECTION ( 'NONE',  ( -0.000000000000000000, -0.000000000000000000, -1.000000000000000000 ) ) ;
#508=ADVANCED_FACE ( 'NONE', ( #14708 ), #11023, .T. ) ;
#540=LINE ( 'NONE', #22618, #14924 ) ;
#555=VERTEX_POINT ( 'NONE', #21228 ) ;
#571=ADVANCED_FACE ( 'NONE', ( #2427 ), #17549, .T. ) ;
#593=CIRCLE ( 'NONE', #14217, 11.00000000000000711 ) ;
#600=AXIS2_PLACEMENT_3D ( 'NONE', #18888, #17417, #17043 ) ;
#618=CARTESIAN_POINT ( 'NONE',  ( 21.13207267780287069, -38.32709852940855910, 12.00000000000000000 ) ) ;
#622=EDGE_CURVE ( 'NONE', #5826, #19489, #1182, .T. ) ;
#623=DIRECTION ( 'NONE',  ( 1.000000000000000000, 0.000000000000000000, 0.000000000000000000 ) ) ;
#627=AXIS2_PLACEMENT_3D ( 'NONE', #21072, #23298, #6451 ) ;
#630=EDGE_CURVE ( 'NONE', #7385, #14193, #9403, .T. ) ;
#638=CIRCLE ( 'NONE', #11898, 2.000000000000000000 ) ;
#639=CARTESIAN_POINT ( 'NONE',  ( -39.00000000000000000, 0.000000000000000000, 11.00000000000000000 ) ) ;
#643=ORIENTED_EDGE ( 'NONE', *, *, #13151, .T. ) ;
#652=AXIS2_PLACEMENT_3D ( 'NONE', #20653, #18823, #22381 ) ;
#654=ORIENTED_EDGE ( 'NONE', *, *, #2684, .F. ) ;
#656=ADVANCED_FACE ( 'NONE', ( #16980 ), #13077, .F. ) ;
#663=ORIENTED_EDGE ( 'NONE', *, *, #15331, .T. ) ;
#666=VERTEX_POINT ( 'NONE', #17096 ) ;
#669=CARTESIAN_POINT ( 'NONE',  ( 33.99999999999998579, 4.999999999999985789, 10.49999999999999822 ) ) ;
#671=VERTEX_POINT ( 'NONE', #20543 ) ;
#672=CARTESIAN_POINT ( 'NONE',  ( -41.00000000000000000, 6.000000000000000888, 11.00000000000000000 ) ) ;
#684=EDGE_CURVE ( 'NONE', #411, #21048, #23857, .T. ) ;
#689=CYLINDRICAL_SURFACE ( 'NONE', #18467, 50.00000000000000000 ) ;
#716=CIRCLE ( 'NONE', #6156, 1.000000000000000888 ) ;
#722=DIRECTION ( 'NONE',  ( 1.000000000000000000, 0.000000000000000000, 0.000000000000000000 ) ) ;
#723=FACE_OUTER_BOUND ( 'NONE', #23290, .T. ) ;
#737=DIRECTION ( 'NONE',  ( 0.5654966663575777819, -0.8247505806839220410, 0.000000000000000000 ) ) ;
#740=ADVANCED_FACE ( 'NONE', ( #18816 ), #2101, .F. ) ;
#741=DIRECTION ( 'NONE',  ( 1.000000000000000000, 1.110223024625155594E-14, 0.000000000000000000 ) ) ;
#758=VERTEX_POINT ( 'NONE', #1015 ) ;
#768=EDGE_CURVE ( 'NONE', #10954, #4131, #21910, .T. ) ;
#776=ORIENTED_EDGE ( 'NONE', *, *, #14281, .F. ) ;
#781=DIRECTION ( 'NONE',  ( 1.000000000000000000, 8.881784197001252323E-16, 0.000000000000000000 ) ) ;
#791=ORIENTED_EDGE ( 'NONE', *, *, #13348, .F. ) ;
#792=ORIENTED_EDGE ( 'NONE', *, *, #2605, .T. ) ;
#794=ORIENTED_EDGE ( 'NONE', *, *, #18251, .T. ) ;
#799=CARTESIAN_POINT ( 'NONE',  ( 42.00000000000000000, 26.82133436441678853, 11.00000000000000000 ) ) ;
#808=AXIS2_PLACEMENT_3D ( 'NONE', #4669, #4301, #12072 ) ;
#817=EDGE_CURVE ( 'NONE', #20489, #21814, #117, .T. ) ;
#819=ORIENTED_EDGE ( 'NONE', *, *, #399, .F. ) ;
#827=CARTESIAN_POINT ( 'NONE',  ( -29.00000000000000000, 29.49999999999999645, 11.50000000000000000 ) ) ;
#834=EDGE_CURVE ( 'NONE', #21352, #8760, #14170, .T. ) ;
#847=CARTESIAN_POINT ( 'NONE',  ( -41.00000000000000000, -6.000000000000000888, 11.00000000000000000 ) ) ;
#848=ORIENTED_EDGE ( 'NONE', *, *, #22737, .T. ) ;
#851=CARTESIAN_POINT ( 'NONE',  ( -20.84999999999999787, 16.67999999999985405, 13.00000000000000178 ) ) ;
#853=CIRCLE ( 'NONE', #13299, 1.000000000000000888 ) ;
#855=DIRECTION ( 'NONE',  ( -0.000000000000000000, -0.000000000000000000, -1.000000000000000000 ) ) ;
#861=CARTESIAN_POINT ( 'NONE',  ( -42.00000000000000000, -6.000000000000000888, 11.00000000000000000 ) ) ;
#870=DIRECTION ( 'NONE',  ( 1.000000000000000000, -2.600433232233976523E-16, 0.000000000000000000 ) ) ;
#876=ORIENTED_EDGE ( 'NONE', *, *, #14081, .T. ) ;
#887=ORIENTED_EDGE ( 'NONE', *, *, #1639, .T. ) ;
#897=TOROIDAL_SURFACE ( 'NONE', #14515, 21.85000000000000142, 1.000000000000000000 ) ;
#900=AXIS2_PLACEMENT_3D ( 'NONE', #7042, #870, #23670 ) ;
#904=CARTESIAN_POINT ( 'NONE',  ( 0.000000000000000000, 0.000000000000000000, 11.00000000000000000 ) ) ;
#907=CARTESIAN_POINT ( 'NONE',  ( -29.00000000000000000, 29.49999999999999645, 12.00000000000000000 ) ) ;
#919=CIRCLE ( 'NONE', #14538, 49.00000000000000000 ) ;
#922=DIRECTION ( 'NONE',  ( -0.000000000000000000, -0.000000000000000000, -1.000000000000000000 ) ) ;
#926=CARTESIAN_POINT ( 'NONE',  ( 41.00000000000000000, 5.999999999999986677, 9.500000000000000000 ) ) ;
#931=CARTESIAN_POINT ( 'NONE',  ( 1.999999999999994449, -45.00000000000000000, 0.000000000000000000 ) ) ;
#933=FACE_OUTER_BOUND ( 'NONE', #2326, .T. ) ;
#935=AXIS2_PLACEMENT_3D ( 'NONE', #16802, #13032, #13266 ) ;
#945=DIRECTION ( 'NONE',  ( -0.000000000000000000, -0.000000000000000000, -1.000000000000000000 ) ) ;
#963=EDGE_CURVE ( 'NONE', #1596, #21975, #18029, .T. ) ;
#974=ORIENTED_EDGE ( 'NONE', *, *, #5929, .T. ) ;
#976=CIRCLE ( 'NONE', #13035, 4.999999999999997335 ) ;
#977=VERTEX_POINT ( 'NONE', #9155 ) ;
#980=DIRECTION ( 'NONE',  ( 0.000000000000000000, 1.000000000000000000, 0.000000000000000000 ) ) ;
#981=CIRCLE ( 'NONE', #16926, 1.000000000000000888 ) ;
#985=AXIS2_PLACEMENT_3D ( 'NONE', #13641, #470, #7655 ) ;
#1000=DIRECTION ( 'NONE',  ( 0.000000000000000000, -0.000000000000000000, -1.000000000000000000 ) ) ;
#1015=CARTESIAN_POINT ( 'NONE',  ( -23.90000000000000213, -29.49999999999999645, 11.50000000000000000 ) ) ;
#1031=FACE_BOUND ( 'NONE', #499, .T. ) ;
#1033=CARTESIAN_POINT ( 'NONE',  ( 1.041919733032276918, 45.00000000000000000, 0.000000000000000000 ) ) ;
#1035=DIRECTION ( 'NONE',  ( -0.000000000000000000, 1.000000000000000000, -0.000000000000000000 ) ) ;
#1036=AXIS2_PLACEMENT_3D ( 'NONE', #1200, #8747, #23760 ) ;
#1042=ORIENTED_EDGE ( 'NONE', *, *, #15791, .F. ) ;
#1044=CARTESIAN_POINT ( 'NONE',  ( -41.00000000000000000, -5.000000000000000888, 10.49999999999999822 ) ) ;
#1050=ORIENTED_EDGE ( 'NONE', *, *, #8866, .T. ) ;
#1056=CARTESIAN_POINT ( 'NONE',  ( 42.00000000000000000, 4.999999999999986677, 10.49999999999999822 ) ) ;
#1057=CIRCLE ( 'NONE', #17789, 5.099999999999996980 ) ;
#1071=ADVANCED_FACE ( 'NONE', ( #13164 ), #19610, .T. ) ;
#1085=DIRECTION ( 'NONE',  ( 0.000000000000000000, 0.000000000000000000, -1.000000000000000000 ) ) ;
#1101=EDGE_LOOP ( 'NONE', ( #10795, #24093, #23817, #6068 ) ) ;
#1102=ORIENTED_EDGE ( 'NONE', *, *, #4855, .F. ) ;
#1117=VERTEX_POINT ( 'NONE', #9366 ) ;
#1123=EDGE_CURVE ( 'NONE', #19436, #145, #9058, .T. ) ;
#1124=LINE ( 'NONE', #15987, #1184 ) ;
#1127=ADVANCED_FACE ( 'NONE', ( #9265 ), #23096, .F. ) ;
#1129=CARTESIAN_POINT ( 'NONE',  ( 42.00000000000000000, -26.82133436441678853, 11.00000000000000000 ) ) ;
#1137=DIRECTION ( 'NONE',  ( -0.000000000000000000, 0.000000000000000000, 1.000000000000000000 ) ) ;
#1152=DIRECTION ( 'NONE',  ( 1.000000000000000000, 0.000000000000000000, 0.000000000000000000 ) ) ;
#1180=DIRECTION ( 'NONE',  ( -0.000000000000000000, -0.000000000000000000, -1.000000000000000000 ) ) ;
#1182=CIRCLE ( 'NONE', #9656, 1.999999999999994449 ) ;
#1184=VECTOR ( 'NONE', #4549, 1000.000000000000000 ) ;
#1187=ADVANCED_FACE ( 'NONE', ( #7670 ), #11312, .T. ) ;
#1189=ORIENTED_EDGE ( 'NONE', *, *, #10741, .F. ) ;
#1190=ORIENTED_EDGE ( 'NONE', *, *, #1629, .F. ) ;
#1200=CARTESIAN_POINT ( 'NONE',  ( -41.00000000000000000, 4.000000000000000888, 8.500000000000000000 ) ) ;
#1208=DIRECTION ( 'NONE',  ( 0.000000000000000000, -1.000000000000000000, 0.000000000000000000 ) ) ;
#1230=CARTESIAN_POINT ( 'NONE',  ( 33.99999999999998579, 3.999999999999985345, 10.49999999999999822 ) ) ;
#1231=VERTEX_POINT ( 'NONE', #23781 ) ;
#1239=CARTESIAN_POINT ( 'NONE',  ( -42.00000000000000000, -4.000000000000000888, 10.49999999999999822 ) ) ;
#1247=DIRECTION ( 'NONE',  ( 0.000000000000000000, 0.000000000000000000, 1.000000000000000000 ) ) ;
#1256=EDGE_LOOP ( 'NONE', ( #10196, #22504, #16988, #19893 ) ) ;
#1258=ADVANCED_FACE ( 'NONE', ( #16086 ), #8994, .F. ) ;
#1262=VECTOR ( 'NONE', #20970, 1000.000000000000000 ) ;
#1264=EDGE_LOOP ( 'NONE', ( #5368, #8367, #12828, #5738 ) ) ;
#1269=DIRECTION ( 'NONE',  ( 0.000000000000000000, 0.000000000000000000, 1.000000000000000000 ) ) ;
#1274=FACE_OUTER_BOUND ( 'NONE', #10623, .T. ) ;
#1280=PLANE ( 'NONE',  #22473 ) ;
#1286=DIRECTION ( 'NONE',  ( 0.000000000000000000, 0.000000000000000000, 1.000000000000000000 ) ) ;
#1292=ORIENTED_EDGE ( 'NONE', *, *, #21074, .T. ) ;
#1306=ORIENTED_EDGE ( 'NONE', *, *, #3440, .T. ) ;
#1316=DIRECTION ( 'NONE',  ( -0.000000000000000000, -0.000000000000000000, 1.000000000000000000 ) ) ;
#1335=CARTESIAN_POINT ( 'NONE',  ( 29.00000000000000000, -29.50000000000000355, 11.00000000000000000 ) ) ;
#1341=FACE_OUTER_BOUND ( 'NONE', #185, .T. ) ;
#1354=CIRCLE ( 'NONE', #15750, 1.000000000000000888 ) ;
#1358=DIRECTION ( 'NONE',  ( -1.000000000000000000, 0.000000000000000000, 0.000000000000000000 ) ) ;
#1362=CARTESIAN_POINT ( 'NONE',  ( -34.00000000000000000, 4.999999999999999112, 10.49999999999999822 ) ) ;
#1364=LINE ( 'NONE', #20019, #16835 ) ;
#1368=CARTESIAN_POINT ( 'NONE',  ( -42.00000000000000000, 6.000000000000000888, 10.49999999999999822 ) ) ;
#1382=ADVANCED_FACE ( 'NONE', ( #2145 ), #9572, .T. ) ;
#1383=DIRECTION ( 'NONE',  ( 1.000000000000000000, 0.000000000000000000, 0.000000000000000000 ) ) ;
#1384=VECTOR ( 'NONE', #10284, 1000.000000000000000 ) ;
#1405=LINE ( 'NONE', #6890, #2438 ) ;
#1409=VERTEX_POINT ( 'NONE', #15169 ) ;
#1418=DIRECTION ( 'NONE',  ( 0.000000000000000000, 0.000000000000000000, 1.000000000000000000 ) ) ;
#1435=ADVANCED_FACE ( 'NONE', ( #6656 ), #10166, .T. ) ;
#1436=DIRECTION ( 'NONE',  ( -0.000000000000000000, 0.000000000000000000, 1.000000000000000000 ) ) ;
#1443=EDGE_CURVE ( 'NONE', #2102, #12778, #15399, .T. ) ;
#1447=EDGE_LOOP ( 'NONE', ( #10380, #22647, #5919, #8431 ) ) ;
#1458=AXIS2_PLACEMENT_3D ( 'NONE', #3926, #9389, #167 ) ;
#1464=EDGE_CURVE ( 'NONE', #14261, #22901, #12181, .T. ) ;
#1476=ORIENTED_EDGE ( 'NONE', *, *, #20075, .T. ) ;
#1484=EDGE_LOOP ( 'NONE', ( #8065, #13351, #5397, #1190 ) ) ;
#1499=ORIENTED_EDGE ( 'NONE', *, *, #11874, .T. ) ;
#1502=ORIENTED_EDGE ( 'NONE', *, *, #12364, .T. ) ;
#1504=CARTESIAN_POINT ( 'NONE',  ( 21.85000000000000497, 16.67999999999999972, 13.00000000000000178 ) ) ;
#1507=VERTEX_POINT ( 'NONE', #14773 ) ;
#1509=FACE_OUTER_BOUND ( 'NONE', #11228, .T. ) ;
#1511=ADVANCED_FACE ( 'NONE', ( #1509 ), #14411, .F. ) ;
#1526=DIRECTION ( 'NONE',  ( -0.000000000000000000, 0.000000000000000000, 1.000000000000000000 ) ) ;
#1532=DIRECTION ( 'NONE',  ( -0.000000000000000000, -0.000000000000000000, -1.000000000000000000 ) ) ;
#1544=ORIENTED_EDGE ( 'NONE', *, *, #8849, .T. ) ;
#1546=EDGE_LOOP ( 'NONE', ( #9703, #16962, #9143, #10092 ) ) ;
#1552=ADVANCED_FACE ( 'NONE', ( #13554 ), #19163, .F. ) ;
#1559=EDGE_CURVE ( 'NONE', #12121, #3740, #20996, .T. ) ;
#1561=ORIENTED_EDGE ( 'NONE', *, *, #19881, .T. ) ;
#1562=CYLINDRICAL_SURFACE ( 'NONE', #8249, 1.000000000000000888 ) ;
#1569=DIRECTION ( 'NONE',  ( -1.000000000000000000, 0.000000000000000000, 0.000000000000000000 ) ) ;
#1579=LINE ( 'NONE', #8996, #7236 ) ;
#1585=ADVANCED_FACE ( 'NONE', ( #4174 ), #8044, .T. ) ;
#1593=DIRECTION ( 'NONE',  ( 1.000000000000000000, 0.000000000000000000, 0.000000000000000000 ) ) ;
#1594=ORIENTED_EDGE ( 'NONE', *, *, #7005, .T. ) ;
#1596=VERTEX_POINT ( 'NONE', #20630 ) ;
#1597=DIRECTION ( 'NONE',  ( 1.000000000000000000, 0.000000000000000000, 0.000000000000000000 ) ) ;
#1600=DIRECTION ( 'NONE',  ( 1.000000000000000000, 0.000000000000000000, 0.000000000000000000 ) ) ;
#1601=DIRECTION ( 'NONE',  ( 1.000000000000000000, 0.000000000000000000, 0.000000000000000000 ) ) ;
#1615=DIRECTION ( 'NONE',  ( -0.000000000000000000, 0.000000000000000000, 1.000000000000000000 ) ) ;
#1621=ORIENTED_EDGE ( 'NONE', *, *, #1998, .F. ) ;
#1624=VECTOR ( 'NONE', #19326, 1000.000000000000000 ) ;
#1629=EDGE_CURVE ( 'NONE', #5218, #11723, #469, .T. ) ;
#1633=ORIENTED_EDGE ( 'NONE', *, *, #14760, .F. ) ;
#1636=VERTEX_POINT ( 'NONE', #17195 ) ;
#1637=CIRCLE ( 'NONE', #4769, 1.000000000000000888 ) ;
#1638=TOROIDAL_SURFACE ( 'NONE', #9853, 5.999999999999999112, 1.000000000000000000 ) ;
#1639=EDGE_CURVE ( 'NONE', #21260, #13716, #19946, .T. ) ;
#1646=CYLINDRICAL_SURFACE ( 'NONE', #3565, 1.000000000000000000 ) ;
#1648=DIRECTION ( 'NONE',  ( -0.000000000000000000, 0.000000000000000000, 1.000000000000000000 ) ) ;
#1649=DIRECTION ( 'NONE',  ( -1.000000000000000000, 0.000000000000000000, 0.000000000000000000 ) ) ;
#1658=AXIS2_PLACEMENT_3D ( 'NONE', #16702, #4265, #6090 ) ;
#1660=TOROIDAL_SURFACE ( 'NONE', #2048, 3.999999999999999112, 1.000000000000000000 ) ;
#1661=PRODUCT_CONTEXT ( 'NONE', #5736, 'mechanical' ) ;
#1662=AXIS2_PLACEMENT_3D ( 'NONE', #23977, #5539, #16524 ) ;
#1663=CARTESIAN_POINT ( 'NONE',  ( 42.00000000000000000, 5.999999999999986677, 9.500000000000000000 ) ) ;
#1666=VERTEX_POINT ( 'NONE', #861 ) ;
#1673=ORIENTED_EDGE ( 'NONE', *, *, #16207, .F. ) ;
#1674=AXIS2_PLACEMENT_3D ( 'NONE', #7386, #5708, #3387 ) ;
#1677=LINE ( 'NONE', #20338, #4789 ) ;
#1680=AXIS2_PLACEMENT_3D ( 'NONE', #18237, #1526, #19837 ) ;
#1683=AXIS2_PLACEMENT_3D ( 'NONE', #21822, #16210, #16425 ) ;
#1684=VECTOR ( 'NONE', #20156, 1000.000000000000227 ) ;
#1685=DIRECTION ( 'NONE',  ( 0.000000000000000000, -1.000000000000000000, 0.000000000000000000 ) ) ;
#1689=ORIENTED_EDGE ( 'NONE', *, *, #14760, .T. ) ;
#1692=ORIENTED_EDGE ( 'NONE', *, *, #21653, .T. ) ;
#1697=VECTOR ( 'NONE', #6460, 1000.000000000000000 ) ;
#1709=CARTESIAN_POINT ( 'NONE',  ( -41.00000000000000000, 6.000000000000000888, 11.00000000000000000 ) ) ;
#1710=LINE ( 'NONE', #20149, #13741 ) ;
#1714=CARTESIAN_POINT ( 'NONE',  ( -34.00000000000000000, -3.851859888774471706E-31, 11.00000000000000000 ) ) ;
#1717=EDGE_CURVE ( 'NONE', #3810, #3246, #9387, .T. ) ;
#1729=CARTESIAN_POINT ( 'NONE',  ( -20.84999999999999787, 16.67999999999985405, 14.50000000000000000 ) ) ;
#1739=CIRCLE ( 'NONE', #13415, 4.000000000000000000 ) ;
#1748=DIRECTION ( 'NONE',  ( 1.000000000000000000, 0.000000000000000000, 0.000000000000000000 ) ) ;
#1749=AXIS2_PLACEMENT_3D ( 'NONE', #13199, #13791, #20552 ) ;
#1763=ORIENTED_EDGE ( 'NONE', *, *, #12525, .T. ) ;
#1767=DIRECTION ( 'NONE',  ( 0.8757121056631642642, 0.4828336235133043886, 0.000000000000000000 ) ) ;
#1773=AXIS2_PLACEMENT_3D ( 'NONE', #14522, #7083, #8670 ) ;
#1778=AXIS2_PLACEMENT_3D ( 'NONE', #3582, #1532, #12969 ) ;
#1784=DIRECTION ( 'NONE',  ( 0.4828336235133042775, 0.8757121056631643752, 0.000000000000000000 ) ) ;
#1789=CIRCLE ( 'NONE', #17764, 4.999999999999997335 ) ;
#1796=CARTESIAN_POINT ( 'NONE',  ( 30.31394790604173295, -39.41330121100981643, 11.00000000000000000 ) ) ;
#1811=AXIS2_PLACEMENT_3D ( 'NONE', #6810, #8966, #22178 ) ;
#1813=VERTEX_POINT ( 'NONE', #22508 ) ;
#1821=AXIS2_PLACEMENT_3D ( 'NONE', #20514, #7782, #20738 ) ;
#1832=FACE_OUTER_BOUND ( 'NONE', #9054, .T. ) ;
#1836=EDGE_CURVE ( 'NONE', #5011, #7495, #302, .T. ) ;
#1844=ORIENTED_EDGE ( 'NONE', *, *, #23123, .T. ) ;
#1845=DIRECTION ( 'NONE',  ( 1.000000000000000000, 0.000000000000000000, 0.000000000000000000 ) ) ;
#1856=DIRECTION ( 'NONE',  ( -0.000000000000000000, -0.000000000000000000, -1.000000000000000000 ) ) ;
#1858=ORIENTED_EDGE ( 'NONE', *, *, #22334, .F. ) ;
#1865=LINE ( 'NONE', #22370, #10979 ) ;
#1871=ORIENTED_EDGE ( 'NONE', *, *, #10492, .F. ) ;
#1873=EDGE_LOOP ( 'NONE', ( #9576, #18180 ) ) ;
#1884=CYLINDRICAL_SURFACE ( 'NONE', #13304, 11.00000000000000711 ) ;
#1886=CARTESIAN_POINT ( 'NONE',  ( -0.9830802669677229932, 45.00000000000000000, 0.000000000000000000 ) ) ;
#1892=DIRECTION ( 'NONE',  ( -0.000000000000000000, -0.000000000000000000, -1.000000000000000000 ) ) ;
#1906=FACE_OUTER_BOUND ( 'NONE', #1447, .T. ) ;
#1912=ORIENTED_EDGE ( 'NONE', *, *, #8849, .F. ) ;
#1914=EDGE_CURVE ( 'NONE', #2972, #11051, #21872, .T. ) ;
#1926=ORIENTED_EDGE ( 'NONE', *, *, #16355, .T. ) ;
#1938=CARTESIAN_POINT ( 'NONE',  ( -41.50000000000000000, 28.80990663662250739, 0.000000000000000000 ) ) ;
#1939=DIRECTION ( 'NONE',  ( 1.000000000000000000, 0.000000000000000000, 0.000000000000000000 ) ) ;
#1954=VECTOR ( 'NONE', #16624, 1000.000000000000000 ) ;
#1961=LINE ( 'NONE', #11218, #119 ) ;
#1962=DIRECTION ( 'NONE',  ( 1.000000000000000000, 0.000000000000000000, 0.000000000000000000 ) ) ;
#1966=DIRECTION ( 'NONE',  ( 1.000000000000000000, 0.000000000000000000, 0.000000000000000000 ) ) ;
#1979=ORIENTED_EDGE ( 'NONE', *, *, #630, .T. ) ;
#1982=CARTESIAN_POINT ( 'NONE',  ( -41.00000000000000000, 0.000000000000000000, 11.00000000000000000 ) ) ;
#1984=DIRECTION ( 'NONE',  ( 0.000000000000000000, 1.000000000000000000, -0.000000000000000000 ) ) ;
#1991=CARTESIAN_POINT ( 'NONE',  ( -34.10000000000000142, -29.49999999999999645, 12.00000000000000000 ) ) ;
#1998=EDGE_CURVE ( 'NONE', #19489, #8713, #8562, .T. ) ;
#1999=ORIENTED_EDGE ( 'NONE', *, *, #12364, .F. ) ;
#2009=ADVANCED_FACE ( 'NONE', ( #14775 ), #18650, .T. ) ;
#2014=CARTESIAN_POINT ( 'NONE',  ( 40.77574956473004875, -27.49633847812775400, 11.00000000000000000 ) ) ;
#2017=ORIENTED_EDGE ( 'NONE', *, *, #19982, .T. ) ;
#2019=ORIENTED_EDGE ( 'NONE', *, *, #15607, .F. ) ;
#2022=CARTESIAN_POINT ( 'NONE',  ( -31.10231664966676846, -45.36128193761570770, 0.000000000000000000 ) ) ;
#2042=DIRECTION ( 'NONE',  ( 0.000000000000000000, -1.000000000000000000, 0.000000000000000000 ) ) ;
#2045=CARTESIAN_POINT ( 'NONE',  ( -41.00000000000000000, 5.000000000000000888, 12.00000000000000000 ) ) ;
#2048=AXIS2_PLACEMENT_3D ( 'NONE', #20013, #463, #13392 ) ;
#2049=VECTOR ( 'NONE', #9640, 1000.000000000000000 ) ;
#2052=DIRECTION ( 'NONE',  ( -1.000000000000000000, 0.000000000000000000, 0.000000000000000000 ) ) ;
#2063=ORIENTED_EDGE ( 'NONE', *, *, #7829, .T. ) ;
#2065=EDGE_CURVE ( 'NONE', #12301, #23300, #19435, .T. ) ;
#2074=CIRCLE ( 'NONE', #7144, 1.999999999999994449 ) ;
#2077=ORIENTED_EDGE ( 'NONE', *, *, #5531, .T. ) ;
#2080=CARTESIAN_POINT ( 'NONE',  ( -3.008080266967722682, 45.00000000000000000, 0.000000000000000000 ) ) ;
#2082=DIRECTION ( 'NONE',  ( 0.000000000000000000, 0.000000000000000000, 1.000000000000000000 ) ) ;
#2085=AXIS2_PLACEMENT_3D ( 'NONE', #1886, #9072, #20426 ) ;
#2089=EDGE_CURVE ( 'NONE', #1507, #20489, #12936, .T. ) ;
#2091=CARTESIAN_POINT ( 'NONE',  ( 41.00000000000000000, -6.000000000000015099, 11.00000000000000000 ) ) ;
#2093=CARTESIAN_POINT ( 'NONE',  ( -42.00000000000000000, 4.000000000000000888, 8.500000000000000000 ) ) ;
#2101=CYLINDRICAL_SURFACE ( 'NONE', #17612, 5.099999999999996980 ) ;
#2102=VERTEX_POINT ( 'NONE', #9277 ) ;
#2106=ORIENTED_EDGE ( 'NONE', *, *, #14113, .T. ) ;
#2114=DIRECTION ( 'NONE',  ( 0.000000000000000000, 0.000000000000000000, 1.000000000000000000 ) ) ;
#2119=CARTESIAN_POINT ( 'NONE',  ( 39.00000000000000000, 29.49999999999999645, 11.00000000000000000 ) ) ;
#2125=CARTESIAN_POINT ( 'NONE',  ( -34.00000000000000000, 3.999999999999999112, 10.49999999999999822 ) ) ;
#2126=EDGE_CURVE ( 'NONE', #2518, #18986, #3835, .T. ) ;
#2143=DIRECTION ( 'NONE',  ( -1.000000000000000000, 0.000000000000000000, 0.000000000000000000 ) ) ;
#2145=FACE_OUTER_BOUND ( 'NONE', #1256, .T. ) ;
#2155=CARTESIAN_POINT ( 'NONE',  ( -41.58578643762692195, 26.57671364288190219, 12.00000000000000000 ) ) ;
#2164=EDGE_LOOP ( 'NONE', ( #11800, #13425, #11091, #19291 ) ) ;
#2167=ORIENTED_EDGE ( 'NONE', *, *, #19047, .T. ) ;
#2187=ADVANCED_FACE ( 'NONE', ( #11322 ), #17083, .T. ) ;
#2201=CARTESIAN_POINT ( 'NONE',  ( -39.00000000000000000, 0.000000000000000000, 12.00000000000000000 ) ) ;
#2215=LINE ( 'NONE', #9998, #23767 ) ;
#2218=EDGE_CURVE ( 'NONE', #7729, #7495, #5394, .T. ) ;
#2228=ORIENTED_EDGE ( 'NONE', *, *, #5965, .F. ) ;
#2240=ADVANCED_FACE ( 'NONE', ( #3172 ), #19796, .F. ) ;
#2244=DIRECTION ( 'NONE',  ( -0.000000000000000000, -0.000000000000000000, -1.000000000000000000 ) ) ;
#2245=DIRECTION ( 'NONE',  ( 0.000000000000000000, 1.000000000000000000, 0.000000000000000000 ) ) ;
#2246=EDGE_LOOP ( 'NONE', ( #21172, #19621, #6418, #15102 ) ) ;
#2250=DIRECTION ( 'NONE',  ( -0.000000000000000000, -0.000000000000000000, -1.000000000000000000 ) ) ;
#2256=VERTEX_POINT ( 'NONE', #21249 ) ;
#2258=FACE_OUTER_BOUND ( 'NONE', #16826, .T. ) ;
#2263=LINE ( 'NONE', #22411, #2886 ) ;
#2269=EDGE_CURVE ( 'NONE', #16460, #1636, #19673, .T. ) ;
#2274=CARTESIAN_POINT ( 'NONE',  ( 19.85000000000000142, 16.67999999999999972, 13.50000000000000178 ) ) ;
#2277=MANIFOLD_SOLID_BREP ( '\X2\00d8\X0\4.0 (4) Diameter Hole1', #8908 ) ;
#2283=ORIENTED_EDGE ( 'NONE', *, *, #24097, .F. ) ;
#2285=EDGE_LOOP ( 'NONE', ( #20924, #18 ) ) ;
#2294=CARTESIAN_POINT ( 'NONE',  ( -2.024999999999999911, -45.00000000000000000, 0.000000000000000000 ) ) ;
#2296=ORIENTED_EDGE ( 'NONE', *, *, #20584, .T. ) ;
#2298=EDGE_CURVE ( 'NONE', #3124, #22790, #13819, .T. ) ;
#2299=EDGE_LOOP ( 'NONE', ( #18222, #654, #11732, #15797 ) ) ;
#2300=CARTESIAN_POINT ( 'NONE',  ( 28.27483331787888332, -41.23752903419610050, 12.00000000000000000 ) ) ;
#2312=CARTESIAN_POINT ( 'NONE',  ( -47.34180362313354351, -5.000000000000002665, 9.500000000000000000 ) ) ;
#2315=DIRECTION ( 'NONE',  ( -0.4828336235133043330, 0.8757121056631641531, 0.000000000000000000 ) ) ;
#2316=ADVANCED_FACE ( 'NONE', ( #14044 ), #9136, .T. ) ;
#2318=TOROIDAL_SURFACE ( 'NONE', #6996, 3.999999999999999112, 1.000000000000000000 ) ;
#2319=DIRECTION ( 'NONE',  ( 0.000000000000000000, -3.469446951953611033E-15, 1.000000000000000000 ) ) ;
#2320=CARTESIAN_POINT ( 'NONE',  ( 40.00000000000000000, 0.000000000000000000, 0.000000000000000000 ) ) ;
#2326=EDGE_LOOP ( 'NONE', ( #22374, #9660, #18680, #10878 ) ) ;
#2337=CYLINDRICAL_SURFACE ( 'NONE', #5475, 5.099999999999996980 ) ;
#2378=VERTEX_POINT ( 'NONE', #7067 ) ;
#2379=DIRECTION ( 'NONE',  ( -0.8757121056631642642, -0.4828336235133043886, 0.000000000000000000 ) ) ;
#2389=FACE_OUTER_BOUND ( 'NONE', #22837, .T. ) ;
#2402=DIRECTION ( 'NONE',  ( 0.000000000000000000, -1.000000000000000000, 0.000000000000000000 ) ) ;
#2404=FACE_OUTER_BOUND ( 'NONE', #13751, .T. ) ;
#2411=LINE ( 'NONE', #11664, #10314 ) ;
#2413=AXIS2_PLACEMENT_3D ( 'NONE', #9252, #19029, #11668 ) ;
#2416=DIRECTION ( 'NONE',  ( -0.000000000000000000, -0.000000000000000000, -1.000000000000000000 ) ) ;
#2417=DIRECTION ( 'NONE',  ( 0.000000000000000000, 0.000000000000000000, 1.000000000000000000 ) ) ;
#2419=CARTESIAN_POINT ( 'NONE',  ( 40.00000000000000000, 29.49999999999999645, 11.00000000000000000 ) ) ;
#2421=ORIENTED_EDGE ( 'NONE', *, *, #23736, .T. ) ;
#2427=FACE_OUTER_BOUND ( 'NONE', #120, .T. ) ;
#2433=CARTESIAN_POINT ( 'NONE',  ( 29.00000000000000000, 29.50000000000000355, 0.000000000000000000 ) ) ;
#2434=CIRCLE ( 'NONE', #1674, 1.000000000000000888 ) ;
#2438=VECTOR ( 'NONE', #3213, 1000.000000000000000 ) ;
#2440=AXIS2_PLACEMENT_3D ( 'NONE', #22894, #3964, #11515 ) ;
#2443=DIRECTION ( 'NONE',  ( 1.000000000000000000, 0.000000000000000000, 0.000000000000000000 ) ) ;
#2451=AXIS2_PLACEMENT_3D ( 'NONE', #11583, #10885, #15230 ) ;
#2452=DIRECTION ( 'NONE',  ( 1.000000000000000000, 0.000000000000000000, 0.000000000000000000 ) ) ;
#2453=VECTOR ( 'NONE', #18838, 1000.000000000000000 ) ;
#2455=CIRCLE ( 'NONE', #8684, 5.999999999999998224 ) ;
#2465=CIRCLE ( 'NONE', #20015, 2.500000000000002220 ) ;
#2467=CARTESIAN_POINT ( 'NONE',  ( 21.85000000000000497, 16.67999999999999972, 13.00000000000000178 ) ) ;
#2477=EDGE_LOOP ( 'NONE', ( #19377, #22413, #1763, #16024 ) ) ;
#2479=CIRCLE ( 'NONE', #10273, 5.099999999999996980 ) ;
#2484=ORIENTED_EDGE ( 'NONE', *, *, #19394, .T. ) ;
#2485=CARTESIAN_POINT ( 'NONE',  ( -29.00000000000000000, 29.49999999999999645, 11.50000000000000000 ) ) ;
#2486=CARTESIAN_POINT ( 'NONE',  ( -27.70933665152130487, -40.41277845351217479, 11.00000000000000000 ) ) ;
#2503=ORIENTED_EDGE ( 'NONE', *, *, #2269, .F. ) ;
#2512=CYLINDRICAL_SURFACE ( 'NONE', #10316, 1.000000000000000888 ) ;
#2518=VERTEX_POINT ( 'NONE', #3867 ) ;
#2523=CARTESIAN_POINT ( 'NONE',  ( -30.31394790604173650, -39.41330121100982353, 12.00000000000000000 ) ) ;
#2539=VECTOR ( 'NONE', #17298, 1000.000000000000000 ) ;
#2546=CARTESIAN_POINT ( 'NONE',  ( 20.85000000000000497, 16.67999999999999972, 13.00000000000000178 ) ) ;
#2552=DIRECTION ( 'NONE',  ( -0.000000000000000000, -0.000000000000000000, 1.000000000000000000 ) ) ;
#2555=ADVANCED_FACE ( 'NONE', ( #5714 ), #11646, .F. ) ;
#2556=ADVANCED_FACE ( 'NONE', ( #2389 ), #22543, .T. ) ;
#2560=VECTOR ( 'NONE', #12453, 1000.000000000000000 ) ;
#2574=AXIS2_PLACEMENT_3D ( 'NONE', #1504, #15768, #6625 ) ;
#2577=ORIENTED_EDGE ( 'NONE', *, *, #21567, .T. ) ;
#2582=ORIENTED_EDGE ( 'NONE', *, *, #19608, .F. ) ;
#2590=DIRECTION ( 'NONE',  ( 1.000000000000000000, -1.156482317317871725E-15, 0.000000000000000000 ) ) ;
#2594=LINE ( 'NONE', #4427, #4721 ) ;
#2600=AXIS2_PLACEMENT_3D ( 'NONE', #12832, #10982, #1748 ) ;
#2605=EDGE_CURVE ( 'NONE', #9181, #1507, #17323, .T. ) ;
#2607=VERTEX_POINT ( 'NONE', #95 ) ;
#2616=LINE ( 'NONE', #11980, #15325 ) ;
#2638=EDGE_CURVE ( 'NONE', #19800, #3497, #7194, .T. ) ;
#2641=ORIENTED_EDGE ( 'NONE', *, *, #18003, .F. ) ;
#2642=DIRECTION ( 'NONE',  ( 0.000000000000000000, 0.000000000000000000, -1.000000000000000000 ) ) ;
#2644=DIRECTION ( 'NONE',  ( 0.000000000000000000, 1.000000000000000000, 0.000000000000000000 ) ) ;
#2650=ORIENTED_EDGE ( 'NONE', *, *, #24032, .F. ) ;
#2664=FACE_OUTER_BOUND ( 'NONE', #20873, .T. ) ;
#2675=VECTOR ( 'NONE', #1856, 1000.000000000000000 ) ;
#2684=EDGE_CURVE ( 'NONE', #16829, #4459, #976, .T. ) ;
#2692=ORIENTED_EDGE ( 'NONE', *, *, #4579, .F. ) ;
#2694=ORIENTED_EDGE ( 'NONE', *, *, #16587, .T. ) ;
#2700=ORIENTED_EDGE ( 'NONE', *, *, #18212, .F. ) ;
#2704=ORIENTED_EDGE ( 'NONE', *, *, #2638, .T. ) ;
#2714=ADVANCED_FACE ( 'NONE', ( #21100 ), #4407, .T. ) ;
#2716=ORIENTED_EDGE ( 'NONE', *, *, #12322, .F. ) ;
#2721=ORIENTED_EDGE ( 'NONE', *, *, #2994, .T. ) ;
#2730=EDGE_LOOP ( 'NONE', ( #3502, #6520, #7114, #1979 ) ) ;
#2738=EDGE_CURVE ( 'NONE', #2772, #6705, #12259, .T. ) ;
#2739=VERTEX_POINT ( 'NONE', #11816 ) ;
#2747=ORIENTED_EDGE ( 'NONE', *, *, #16877, .T. ) ;
#2751=ORIENTED_EDGE ( 'NONE', *, *, #2065, .F. ) ;
#2755=CARTESIAN_POINT ( 'NONE',  ( 2.454813078130514813E-15, 16.67999999999999972, 14.50000000000000000 ) ) ;
#2757=EDGE_CURVE ( 'NONE', #16379, #11259, #7580, .T. ) ;
#2772=VERTEX_POINT ( 'NONE', #19785 ) ;
#2773=LINE ( 'NONE', #23163, #23195 ) ;
#2801=LINE ( 'NONE', #19284, #24037 ) ;
#2803=DIRECTION ( 'NONE',  ( -0.000000000000000000, 0.000000000000000000, 1.000000000000000000 ) ) ;
#2814=CARTESIAN_POINT ( 'NONE',  ( 28.27483331787887977, 41.23752903419610760, 12.00000000000000000 ) ) ;
#2815=EDGE_CURVE ( 'NONE', #8713, #9925, #5707, .T. ) ;
#2842=CARTESIAN_POINT ( 'NONE',  ( -40.77574956473004875, 27.49633847812775400, 11.00000000000000000 ) ) ;
#2844=CIRCLE ( 'NONE', #2451, 5.099999999999996980 ) ;
#2863=AXIS2_PLACEMENT_3D ( 'NONE', #17003, #11356, #306 ) ;
#2870=DIRECTION ( 'NONE',  ( 1.000000000000000000, 3.469446951953611822E-15, 0.000000000000000000 ) ) ;
#2875=DIRECTION ( 'NONE',  ( -1.000000000000000000, 0.000000000000000000, 0.000000000000000000 ) ) ;
#2878=VECTOR ( 'NONE', #18767, 1000.000000000000000 ) ;
#2879=ADVANCED_FACE ( 'NONE', ( #9000 ), #14033, .F. ) ;
#2880=EDGE_CURVE ( 'NONE', #7495, #18986, #18183, .T. ) ;
#2886=VECTOR ( 'NONE', #13356, 1000.000000000000000 ) ;
#2895=AXIS2_PLACEMENT_3D ( 'NONE', #13771, #10088, #21219 ) ;
#2904=AXIS2_PLACEMENT_3D ( 'NONE', #6971, #10732, #12333 ) ;
#2909=ORIENTED_EDGE ( 'NONE', *, *, #19459, .F. ) ;
#2915=DIRECTION ( 'NONE',  ( 1.000000000000000000, 0.000000000000000000, 0.000000000000000000 ) ) ;
#2920=ORIENTED_EDGE ( 'NONE', *, *, #6933, .F. ) ;
#2927=AXIS2_PLACEMENT_3D ( 'NONE', #15073, #20953, #4237 ) ;
#2933=CARTESIAN_POINT ( 'NONE',  ( -28.27483331787888332, -41.23752903419610050, 11.00000000000000000 ) ) ;
#2937=CARTESIAN_POINT ( 'NONE',  ( -0.9830802669677229932, 45.00000000000000000, 3.000000000000002665 ) ) ;
#2938=DIRECTION ( 'NONE',  ( 0.000000000000000000, 0.000000000000000000, -1.000000000000000000 ) ) ;
#2945=DIRECTION ( 'NONE',  ( -0.000000000000000000, -0.000000000000000000, -1.000000000000000000 ) ) ;
#2947=DIRECTION ( 'NONE',  ( -0.000000000000000000, -0.000000000000000000, 1.000000000000000000 ) ) ;
#2952=CIRCLE ( 'NONE', #11933, 1.000000000000000888 ) ;
#2960=CARTESIAN_POINT ( 'NONE',  ( 29.00000000000000000, -29.50000000000000355, 0.000000000000000000 ) ) ;
#2963=CARTESIAN_POINT ( 'NONE',  ( 29.00000000000000000, 29.50000000000000355, 0.000000000000000000 ) ) ;
#2972=VERTEX_POINT ( 'NONE', #16796 ) ;
#2974=EDGE_CURVE ( 'NONE', #9763, #3076, #7406, .T. ) ;
#2975=FACE_OUTER_BOUND ( 'NONE', #10293, .T. ) ;
#2981=DIRECTION ( 'NONE',  ( 0.000000000000000000, -0.000000000000000000, -1.000000000000000000 ) ) ;
#2994=EDGE_CURVE ( 'NONE', #12373, #430, #4119, .T. ) ;
#2996=EDGE_CURVE ( 'NONE', #19937, #1409, #4627, .T. ) ;
#3000=CARTESIAN_POINT ( 'NONE',  ( -39.00000000000000000, 28.80990663662251805, 11.00000000000000000 ) ) ;
#3008=DIRECTION ( 'NONE',  ( -0.000000000000000000, -0.000000000000000000, -1.000000000000000000 ) ) ;
#3011=CARTESIAN_POINT ( 'NONE',  ( 21.85000000000000497, -16.67999999999999616, 13.00000000000000178 ) ) ;
#3014=CYLINDRICAL_SURFACE ( 'NONE', #3948, 1.999999999999994449 ) ;
#3030=EDGE_CURVE ( 'NONE', #21260, #23989, #462, .T. ) ;
#3031=DIRECTION ( 'NONE',  ( -0.000000000000000000, -0.000000000000000000, -1.000000000000000000 ) ) ;
#3036=DIRECTION ( 'NONE',  ( 0.8757121056631640421, 0.4828336235133042775, 0.000000000000000000 ) ) ;
#3039=DIRECTION ( 'NONE',  ( 0.000000000000000000, 0.000000000000000000, 1.000000000000000000 ) ) ;
#3042=DIRECTION ( 'NONE',  ( -0.000000000000000000, 0.000000000000000000, -1.000000000000000000 ) ) ;
#3043=DIRECTION ( 'NONE',  ( -0.000000000000000000, 0.000000000000000000, 1.000000000000000000 ) ) ;
#3053=VECTOR ( 'NONE', #6634, 1000.000000000000227 ) ;
#3057=DIRECTION ( 'NONE',  ( -0.000000000000000000, -0.000000000000000000, -1.000000000000000000 ) ) ;
#3068=LINE ( 'NONE', #2814, #20650 ) ;
#3069=ORIENTED_EDGE ( 'NONE', *, *, #1123, .T. ) ;
#3070=PLANE ( 'NONE',  #7996 ) ;
#3071=ORIENTED_EDGE ( 'NONE', *, *, #19413, .F. ) ;
#3076=VERTEX_POINT ( 'NONE', #15197 ) ;
#3079=DIRECTION ( 'NONE',  ( 0.000000000000000000, 0.000000000000000000, 1.000000000000000000 ) ) ;
#3088=DIRECTION ( 'NONE',  ( 0.8757121056631640421, -0.4828336235133042775, 0.000000000000000000 ) ) ;
#3095=ORIENTED_EDGE ( 'NONE', *, *, #14707, .F. ) ;
#3106=FACE_OUTER_BOUND ( 'NONE', #13307, .T. ) ;
#3117=DIRECTION ( 'NONE',  ( -0.000000000000000000, -0.000000000000000000, 1.000000000000000000 ) ) ;
#3124=VERTEX_POINT ( 'NONE', #10560 ) ;
#3126=VERTEX_POINT ( 'NONE', #5090 ) ;
#3155=ORIENTED_EDGE ( 'NONE', *, *, #10365, .T. ) ;
#3159=ORIENTED_EDGE ( 'NONE', *, *, #3474, .T. ) ;
#3162=DIRECTION ( 'NONE',  ( 0.000000000000000000, 0.000000000000000000, -1.000000000000000000 ) ) ;
#3170=AXIS2_PLACEMENT_3D ( 'NONE', #2022, #9446, #22426 ) ;
#3172=FACE_OUTER_BOUND ( 'NONE', #20099, .T. ) ;
#3176=FACE_OUTER_BOUND ( 'NONE', #9364, .T. ) ;
#3183=CARTESIAN_POINT ( 'NONE',  ( -29.00000000000000000, 29.49999999999999645, 12.00000000000000000 ) ) ;
#3193=ORIENTED_EDGE ( 'NONE', *, *, #2815, .F. ) ;
#3196=DIRECTION ( 'NONE',  ( -0.000000000000000000, -0.000000000000000000, -1.000000000000000000 ) ) ;
#3204=CIRCLE ( 'NONE', #489, 1.000000000000000888 ) ;
#3208=CIRCLE ( 'NONE', #1662, 5.999999999999998224 ) ;
#3213=DIRECTION ( 'NONE',  ( 0.000000000000000000, 1.000000000000000000, 0.000000000000000000 ) ) ;
#3216=VERTEX_POINT ( 'NONE', #16063 ) ;
#3217=AXIS2_PLACEMENT_3D ( 'NONE', #2960, #1137, #4564 ) ;
#3218=LINE ( 'NONE', #21888, #13905 ) ;
#3226=VERTEX_POINT ( 'NONE', #12406 ) ;
#3236=LINE ( 'NONE', #9071, #6629 ) ;
#3237=EDGE_CURVE ( 'NONE', #21962, #21867, #22285, .T. ) ;
#3238=DIRECTION ( 'NONE',  ( -1.000000000000000000, 0.000000000000000000, 0.000000000000000000 ) ) ;
#3246=VERTEX_POINT ( 'NONE', #22179 ) ;
#3252=ORIENTED_EDGE ( 'NONE', *, *, #21530, .T. ) ;
#3256=CARTESIAN_POINT ( 'NONE',  ( -40.29291594121673370, 26.62062637246459929, 12.00000000000000000 ) ) ;
#3257=AXIS2_PLACEMENT_3D ( 'NONE', #23794, #10485, #14499 ) ;
#3260=VERTEX_POINT ( 'NONE', #20688 ) ;
#3268=ADVANCED_FACE ( 'NONE', ( #5702, #7152 ), #11262, .T. ) ;
#3291=AXIS2_PLACEMENT_3D ( 'NONE', #19595, #1286, #12484 ) ;
#3307=TOROIDAL_SURFACE ( 'NONE', #8362, 5.999999999999999112, 1.000000000000000000 ) ;
#3311=AXIS2_PLACEMENT_3D ( 'NONE', #23174, #10458, #6457 ) ;
#3324=CIRCLE ( 'NONE', #13844, 11.00000000000001066 ) ;
#3330=CARTESIAN_POINT ( 'NONE',  ( 34.10000000000000142, -29.50000000000000355, 12.00000000000000000 ) ) ;
#3345=EDGE_CURVE ( 'NONE', #4241, #21197, #14590, .T. ) ;
#3348=EDGE_CURVE ( 'NONE', #16364, #555, #12463, .T. ) ;
#3356=ORIENTED_EDGE ( 'NONE', *, *, #7133, .T. ) ;
#3371=AXIS2_PLACEMENT_3D ( 'NONE', #20903, #17216, #7806 ) ;
#3383=LINE ( 'NONE', #6928, #4540 ) ;
#3387=DIRECTION ( 'NONE',  ( 0.000000000000000000, 0.000000000000000000, 1.000000000000000000 ) ) ;
#3388=EDGE_LOOP ( 'NONE', ( #2421, #8561, #15254, #22546 ) ) ;
#3397=ORIENTED_EDGE ( 'NONE', *, *, #18435, .F. ) ;
#3399=CARTESIAN_POINT ( 'NONE',  ( -20.99999999999999645, -29.49999999999999645, 11.50000000000000000 ) ) ;
#3402=ORIENTED_EDGE ( 'NONE', *, *, #14628, .F. ) ;
#3429=CARTESIAN_POINT ( 'NONE',  ( 2.454813078130514813E-15, -16.67999999999999972, 13.00000000000000178 ) ) ;
#3438=EDGE_CURVE ( 'NONE', #4459, #9207, #9635, .T. ) ;
#3440=EDGE_CURVE ( 'NONE', #21048, #11189, #22142, .T. ) ;
#3448=DIRECTION ( 'NONE',  ( 0.000000000000000000, 0.000000000000000000, -1.000000000000000000 ) ) ;
#3452=ORIENTED_EDGE ( 'NONE', *, *, #11949, .F. ) ;
#3459=EDGE_CURVE ( 'NONE', #671, #5218, #17045, .T. ) ;
#3473=CARTESIAN_POINT ( 'NONE',  ( -29.00000000000000000, 29.49999999999999645, 11.50000000000000000 ) ) ;
#3474=EDGE_CURVE ( 'NONE', #16460, #7598, #716, .T. ) ;
#3495=DIRECTION ( 'NONE',  ( 1.000000000000000000, 0.000000000000000000, 0.000000000000000000 ) ) ;
#3497=VERTEX_POINT ( 'NONE', #7384 ) ;
#3501=VECTOR ( 'NONE', #21182, 1000.000000000000000 ) ;
#3502=ORIENTED_EDGE ( 'NONE', *, *, #9138, .F. ) ;
#3511=EDGE_CURVE ( 'NONE', #17642, #8062, #17452, .T. ) ;
#3514=ORIENTED_EDGE ( 'NONE', *, *, #6926, .T. ) ;
#3518=CARTESIAN_POINT ( 'NONE',  ( -39.00000000000000711, 29.49999999999999645, 12.00000000000000000 ) ) ;
#3522=CIRCLE ( 'NONE', #12838, 1.500000000000001332 ) ;
#3537=ADVANCED_FACE ( 'NONE', ( #24000 ), #7328, .T. ) ;
#3550=EDGE_LOOP ( 'NONE', ( #16182, #4664, #18580, #21636 ) ) ;
#3560=EDGE_LOOP ( 'NONE', ( #10483, #5200, #15187, #12381 ) ) ;
#3565=AXIS2_PLACEMENT_3D ( 'NONE', #3586, #14697, #5185 ) ;
#3567=ORIENTED_EDGE ( 'NONE', *, *, #7832, .F. ) ;
#3573=DIRECTION ( 'NONE',  ( 0.000000000000000000, 1.000000000000000000, 0.000000000000000000 ) ) ;
#3578=AXIS2_PLACEMENT_3D ( 'NONE', #380, #16828, #3912 ) ;
#3582=CARTESIAN_POINT ( 'NONE',  ( -29.00000000000000000, -29.49999999999999645, 11.50000000000000000 ) ) ;
#3585=FACE_OUTER_BOUND ( 'NONE', #7462, .T. ) ;
#3586=CARTESIAN_POINT ( 'NONE',  ( 41.00000000000000000, -1.387778780781445676E-14, 8.500000000000000000 ) ) ;
#3589=DIRECTION ( 'NONE',  ( -1.000000000000000000, 0.000000000000000000, 0.000000000000000000 ) ) ;
#3601=CARTESIAN_POINT ( 'NONE',  ( 20.64923905428956630, 37.45138642374539728, 11.00000000000000000 ) ) ;
#3613=CARTESIAN_POINT ( 'NONE',  ( 0.000000000000000000, -45.00000000000000000, 3.000000000000002665 ) ) ;
#3614=CARTESIAN_POINT ( 'NONE',  ( 29.00000000000000000, 29.50000000000000355, 12.00000000000000000 ) ) ;
#3618=TOROIDAL_SURFACE ( 'NONE', #23509, 49.00000000000000000, 1.000000000000000000 ) ;
#3627=LINE ( 'NONE', #6943, #10230 ) ;
#3632=EDGE_LOOP ( 'NONE', ( #7754, #3159, #9317, #18659 ) ) ;
#3640=VECTOR ( 'NONE', #9641, 1000.000000000000000 ) ;
#3686=AXIS2_PLACEMENT_3D ( 'NONE', #22286, #11390, #5563 ) ;
#3698=ORIENTED_EDGE ( 'NONE', *, *, #834, .F. ) ;
#3700=VECTOR ( 'NONE', #22783, 1000.000000000000000 ) ;
#3701=ORIENTED_EDGE ( 'NONE', *, *, #15724, .T. ) ;
#3705=VERTEX_POINT ( 'NONE', #15171 ) ;
#3727=CIRCLE ( 'NONE', #13048, 5.999999999999998224 ) ;
#3740=VERTEX_POINT ( 'NONE', #19475 ) ;
#3742=LINE ( 'NONE', #20579, #10740 ) ;
#3743=DIRECTION ( 'NONE',  ( 0.000000000000000000, 0.000000000000000000, 1.000000000000000000 ) ) ;
#3754=DIRECTION ( 'NONE',  ( -0.4828336235133042775, -0.8757121056631643752, 0.000000000000000000 ) ) ;
#3762=VERTEX_POINT ( 'NONE', #19726 ) ;
#3769=ORIENTED_EDGE ( 'NONE', *, *, #963, .F. ) ;
#3778=FACE_OUTER_BOUND ( 'NONE', #3992, .T. ) ;
#3780=DIRECTION ( 'NONE',  ( -0.000000000000000000, -0.000000000000000000, -1.000000000000000000 ) ) ;
#3785=DIRECTION ( 'NONE',  ( 0.000000000000000000, 0.000000000000000000, 1.000000000000000000 ) ) ;
#3786=EDGE_CURVE ( 'NONE', #3740, #13716, #9935, .T. ) ;
#3795=CARTESIAN_POINT ( 'NONE',  ( -23.90000000000000213, 29.49999999999999645, 0.000000000000000000 ) ) ;
#3799=ORIENTED_EDGE ( 'NONE', *, *, #18905, .T. ) ;
#3810=VERTEX_POINT ( 'NONE', #15925 ) ;
#3813=CARTESIAN_POINT ( 'NONE',  ( 41.50000000000000000, -28.80990663662250739, 11.00000000000000000 ) ) ;
#3835=CIRCLE ( 'NONE', #20981, 1.000000000000000000 ) ;
#3839=DIRECTION ( 'NONE',  ( 1.000000000000000000, 0.000000000000000000, 0.000000000000000000 ) ) ;
#3856=DIRECTION ( 'NONE',  ( -0.8757121056631641531, 0.4828336235133042775, 0.000000000000000000 ) ) ;
#3867=CARTESIAN_POINT ( 'NONE',  ( -42.00000000000000000, -4.000000000000000888, 8.500000000000000000 ) ) ;
#3877=ORIENTED_EDGE ( 'NONE', *, *, #5504, .T. ) ;
#3882=LINE ( 'NONE', #237, #9864 ) ;
#3893=CARTESIAN_POINT ( 'NONE',  ( 42.00000000000000000, 26.82133436441678853, 12.00000000000000000 ) ) ;
#3897=ORIENTED_EDGE ( 'NONE', *, *, #8866, .F. ) ;
#3899=ORIENTED_EDGE ( 'NONE', *, *, #4858, .F. ) ;
#3906=LINE ( 'NONE', #2201, #16568 ) ;
#3907=CARTESIAN_POINT ( 'NONE',  ( 0.000000000000000000, 0.000000000000000000, 12.00000000000000000 ) ) ;
#3910=EDGE_LOOP ( 'NONE', ( #23048, #18492 ) ) ;
#3912=DIRECTION ( 'NONE',  ( 1.000000000000000000, 0.000000000000000000, 0.000000000000000000 ) ) ;
#3922=DIRECTION ( 'NONE',  ( 1.000000000000000000, 0.000000000000000000, 0.000000000000000000 ) ) ;
#3926=CARTESIAN_POINT ( 'NONE',  ( 2.454813078130514813E-15, -16.67999999999999972, 13.50000000000000178 ) ) ;
#3927=DIRECTION ( 'NONE',  ( -0.000000000000000000, -0.000000000000000000, -1.000000000000000000 ) ) ;
#3937=LINE ( 'NONE', #5887, #4024 ) ;
#3948=AXIS2_PLACEMENT_3D ( 'NONE', #15674, #13989, #3238 ) ;
#3950=DIRECTION ( 'NONE',  ( 0.000000000000000000, 0.000000000000000000, -1.000000000000000000 ) ) ;
#3953=LINE ( 'NONE', #12099, #22358 ) ;
#3956=VERTEX_POINT ( 'NONE', #14431 ) ;
#3963=ORIENTED_EDGE ( 'NONE', *, *, #15057, .T. ) ;
#3964=DIRECTION ( 'NONE',  ( 0.000000000000000000, -0.000000000000000000, -1.000000000000000000 ) ) ;
#3969=CYLINDRICAL_SURFACE ( 'NONE', #14194, 1.500000000000001332 ) ;
#3972=DIRECTION ( 'NONE',  ( 1.000000000000000000, 0.000000000000000000, 0.000000000000000000 ) ) ;
#3982=DIRECTION ( 'NONE',  ( 0.000000000000000000, -1.000000000000000000, 0.000000000000000000 ) ) ;
#3984=AXIS2_PLACEMENT_3D ( 'NONE', #2467, #291, #17348 ) ;
#3986=AXIS2_PLACEMENT_3D ( 'NONE', #16012, #21282, #1152 ) ;
#3992=EDGE_LOOP ( 'NONE', ( #20327, #20719, #11977 ) ) ;
#4001=AXIS2_PLACEMENT_3D ( 'NONE', #16813, #20988, #13414 ) ;
#4002=AXIS2_PLACEMENT_3D ( 'NONE', #17453, #14154, #21488 ) ;
#4024=VECTOR ( 'NONE', #14688, 1000.000000000000000 ) ;
#4027=AXIS2_PLACEMENT_3D ( 'NONE', #12417, #20700, #20838 ) ;
#4034=DIRECTION ( 'NONE',  ( -0.000000000000000000, 0.000000000000000000, 1.000000000000000000 ) ) ;
#4040=EDGE_LOOP ( 'NONE', ( #10842, #1633, #18628, #7371 ) ) ;
#4042=CIRCLE ( 'NONE', #10266, 8.000000000000003553 ) ;
#4046=AXIS2_PLACEMENT_3D ( 'NONE', #3000, #6541, #23382 ) ;
#4047=CARTESIAN_POINT ( 'NONE',  ( -29.00000000000000000, -29.49999999999999645, 11.50000000000000000 ) ) ;
#4071=CIRCLE ( 'NONE', #16137, 0.9999999999999994449 ) ;
#4076=FACE_OUTER_BOUND ( 'NONE', #3550, .T. ) ;
#4082=LINE ( 'NONE', #1991, #20024 ) ;
#4096=ADVANCED_FACE ( 'NONE', ( #5890 ), #8094, .F. ) ;
#4098=AXIS2_PLACEMENT_3D ( 'NONE', #21575, #3031, #8610 ) ;
#4099=ORIENTED_EDGE ( 'NONE', *, *, #22476, .F. ) ;
#4110=DIRECTION ( 'NONE',  ( 0.000000000000000000, -0.000000000000000000, -1.000000000000000000 ) ) ;
#4119=CIRCLE ( 'NONE', #22431, 21.85000000000000142 ) ;
#4131=VERTEX_POINT ( 'NONE', #9764 ) ;
#4135=AXIS2_PLACEMENT_3D ( 'NONE', #11872, #7830, #9917 ) ;
#4155=CARTESIAN_POINT ( 'NONE',  ( -37.00000000000000711, 29.49999999999999645, 12.00000000000000000 ) ) ;
#4159=VERTEX_POINT ( 'NONE', #5670 ) ;
#4174=FACE_OUTER_BOUND ( 'NONE', #21746, .T. ) ;
#4175=ADVANCED_FACE ( 'NONE', ( #4076 ), #16690, .F. ) ;
#4180=DIRECTION ( 'NONE',  ( 1.000000000000000000, 2.600433232233976523E-16, -0.000000000000000000 ) ) ;
#4186=DIRECTION ( 'NONE',  ( 1.000000000000000000, -2.600433232233976523E-16, -0.000000000000000000 ) ) ;
#4203=DIRECTION ( 'NONE',  ( 0.000000000000000000, 1.000000000000000000, 0.000000000000000000 ) ) ;
#4204=FACE_BOUND ( 'NONE', #16851, .T. ) ;
#4206=CARTESIAN_POINT ( 'NONE',  ( 23.90000000000000568, 29.50000000000000355, 12.00000000000000000 ) ) ;
#4216=DIRECTION ( 'NONE',  ( -1.000000000000000000, 0.000000000000000000, 0.000000000000000000 ) ) ;
#4217=ORIENTED_EDGE ( 'NONE', *, *, #14565, .T. ) ;
#4232=ORIENTED_EDGE ( 'NONE', *, *, #14831, .T. ) ;
#4233=CARTESIAN_POINT ( 'NONE',  ( -41.00000000000000000, 4.000000000000000888, 9.500000000000000000 ) ) ;
#4237=DIRECTION ( 'NONE',  ( 0.000000000000000000, 0.000000000000000000, -1.000000000000000000 ) ) ;
#4241=VERTEX_POINT ( 'NONE', #4313 ) ;
#4258=ADVANCED_FACE ( 'NONE', ( #1031, #2975, #23359, #17227, #8184, #6389 ), #17362, .T. ) ;
#4265=DIRECTION ( 'NONE',  ( 0.000000000000000000, 0.000000000000000000, 1.000000000000000000 ) ) ;
#4301=DIRECTION ( 'NONE',  ( -0.000000000000000000, 0.000000000000000000, 1.000000000000000000 ) ) ;
#4313=CARTESIAN_POINT ( 'NONE',  ( -40.77574956473004164, -27.49633847812775755, 11.00000000000000000 ) ) ;
#4324=CARTESIAN_POINT ( 'NONE',  ( 42.00000000000000000, 26.82133436441678853, 0.000000000000000000 ) ) ;
#4332=ORIENTED_EDGE ( 'NONE', *, *, #20597, .T. ) ;
#4339=AXIS2_PLACEMENT_3D ( 'NONE', #12061, #19793, #21370 ) ;
#4369=EDGE_CURVE ( 'NONE', #7962, #16829, #2263, .T. ) ;
#4372=DIRECTION ( 'NONE',  ( 0.000000000000000000, -0.000000000000000000, 1.000000000000000000 ) ) ;
#4374=DIRECTION ( 'NONE',  ( -2.600433232233976523E-16, -1.000000000000000000, 0.000000000000000000 ) ) ;
#4377=FACE_OUTER_BOUND ( 'NONE', #21705, .T. ) ;
#4392=ORIENTED_EDGE ( 'NONE', *, *, #9196, .F. ) ;
#4404=VECTOR ( 'NONE', #14729, 1000.000000000000000 ) ;
#4407=PLANE ( 'NONE',  #7958 ) ;
#4409=AXIS2_PLACEMENT_3D ( 'NONE', #6047, #20939, #17016 ) ;
#4412=ORIENTED_EDGE ( 'NONE', *, *, #4935, .T. ) ;
#4423=ORIENTED_EDGE ( 'NONE', *, *, #5043, .F. ) ;
#4424=ADVANCED_FACE ( 'NONE', ( #17618 ), #689, .T. ) ;
#4427=CARTESIAN_POINT ( 'NONE',  ( -42.00000000000000000, -5.000000000000000888, 11.00000000000000000 ) ) ;
#4436=DIRECTION ( 'NONE',  ( 0.000000000000000000, -0.000000000000000000, -1.000000000000000000 ) ) ;
#4449=ORIENTED_EDGE ( 'NONE', *, *, #9092, .T. ) ;
#4455=PLANE ( 'NONE',  #17294 ) ;
#4457=ORIENTED_EDGE ( 'NONE', *, *, #17541, .F. ) ;
#4459=VERTEX_POINT ( 'NONE', #21418 ) ;
#4465=EDGE_CURVE ( 'NONE', #12301, #2256, #12984, .T. ) ;
#4469=ORIENTED_EDGE ( 'NONE', *, *, #443, .F. ) ;
#4478=DIRECTION ( 'NONE',  ( -1.000000000000000000, 0.000000000000000000, 0.000000000000000000 ) ) ;
#4487=DIRECTION ( 'NONE',  ( -1.000000000000000000, -2.600433232233976523E-16, -0.000000000000000000 ) ) ;
#4489=AXIS2_PLACEMENT_3D ( 'NONE', #19264, #17423, #722 ) ;
#4491=AXIS2_PLACEMENT_3D ( 'NONE', #8874, #1685, #14832 ) ;
#4497=FACE_OUTER_BOUND ( 'NONE', #17667, .T. ) ;
#4498=ORIENTED_EDGE ( 'NONE', *, *, #17594, .F. ) ;
#4502=ORIENTED_EDGE ( 'NONE', *, *, #19031, .F. ) ;
#4506=VERTEX_POINT ( 'NONE', #12111 ) ;
#4515=CARTESIAN_POINT ( 'NONE',  ( 33.99999999999998579, 5.999999999999985789, 11.00000000000000000 ) ) ;
#4518=CARTESIAN_POINT ( 'NONE',  ( 47.34180362313352930, -5.000000000000016875, 9.500000000000000000 ) ) ;
#4520=EDGE_CURVE ( 'NONE', #21802, #7385, #15921, .T. ) ;
#4521=DIRECTION ( 'NONE',  ( 0.000000000000000000, 0.000000000000000000, 1.000000000000000000 ) ) ;
#4526=ORIENTED_EDGE ( 'NONE', *, *, #17397, .F. ) ;
#4540=VECTOR ( 'NONE', #3036, 1000.000000000000227 ) ;
#4546=CARTESIAN_POINT ( 'NONE',  ( -41.00000000000000000, 6.000000000000000888, 12.00000000000000000 ) ) ;
#4548=VECTOR ( 'NONE', #12950, 1000.000000000000000 ) ;
#4549=DIRECTION ( 'NONE',  ( -0.000000000000000000, -0.000000000000000000, -1.000000000000000000 ) ) ;
#4564=DIRECTION ( 'NONE',  ( 1.000000000000000000, 0.000000000000000000, 0.000000000000000000 ) ) ;
#4574=EDGE_CURVE ( 'NONE', #3226, #12189, #18079, .T. ) ;
#4579=EDGE_CURVE ( 'NONE', #17534, #3076, #12220, .T. ) ;
#4582=( BOUNDED_CURVE ( )  B_SPLINE_CURVE ( 3, ( #22808, #8132, #17169, #15095 ),
 .UNSPECIFIED., .F., .T. ) 
 B_SPLINE_CURVE_WITH_KNOTS ( ( 4, 4 ),
 ( 3.141592653589793116, 4.712388980384691450 ),
 .UNSPECIFIED. ) 
 CURVE ( )  GEOMETRIC_REPRESENTATION_ITEM ( )  RATIONAL_B_SPLINE_CURVE ( ( 1.000000000000000000, 0.8047378541243646044, 0.8047378541243646044, 1.000000000000000000 ) ) 
 REPRESENTATION_ITEM ( '' )  );
#4593=ORIENTED_EDGE ( 'NONE', *, *, #11991, .T. ) ;
#4598=ORIENTED_EDGE ( 'NONE', *, *, #21097, .T. ) ;
#4621=ORIENTED_EDGE ( 'NONE', *, *, #16613, .T. ) ;
#4626=DIRECTION ( 'NONE',  ( 1.000000000000000000, 0.000000000000000000, 0.000000000000000000 ) ) ;
#4627=LINE ( 'NONE', #17165, #20859 ) ;
#4648=DIRECTION ( 'NONE',  ( -0.8757121056631640421, -0.4828336235133042775, 0.000000000000000000 ) ) ;
#4664=ORIENTED_EDGE ( 'NONE', *, *, #18556, .T. ) ;
#4668=ORIENTED_EDGE ( 'NONE', *, *, #8058, .F. ) ;
#4669=CARTESIAN_POINT ( 'NONE',  ( -41.50000000000000000, -28.80990663662250739, 0.000000000000000000 ) ) ;
#4670=CARTESIAN_POINT ( 'NONE',  ( -42.00000000000000000, -6.000000000000000888, 10.49999999999999822 ) ) ;
#4680=AXIS2_PLACEMENT_3D ( 'NONE', #847, #980, #15589 ) ;
#4694=DIRECTION ( 'NONE',  ( -0.000000000000000000, 0.000000000000000000, -1.000000000000000000 ) ) ;
#4700=EDGE_CURVE ( 'NONE', #8062, #21512, #12076, .T. ) ;
#4701=AXIS2_PLACEMENT_3D ( 'NONE', #8162, #15605, #5427 ) ;
#4710=CARTESIAN_POINT ( 'NONE',  ( 34.10000000000000142, 29.50000000000000355, 12.00000000000000000 ) ) ;
#4713=DIRECTION ( 'NONE',  ( 0.000000000000000000, 0.000000000000000000, -1.000000000000000000 ) ) ;
#4714=CARTESIAN_POINT ( 'NONE',  ( 40.00000000000000000, 0.000000000000000000, 12.00000000000000000 ) ) ;
#4719=DIRECTION ( 'NONE',  ( -0.000000000000000000, -1.000000000000000000, -0.000000000000000000 ) ) ;
#4721=VECTOR ( 'NONE', #20899, 1000.000000000000000 ) ;
#4723=CARTESIAN_POINT ( 'NONE',  ( -20.99999999999999645, -29.49999999999999645, 12.00000000000000000 ) ) ;
#4727=LINE ( 'NONE', #14223, #16392 ) ;
#4740=DIRECTION ( 'NONE',  ( 1.000000000000000000, 0.000000000000000000, 0.000000000000000000 ) ) ;
#4742=EDGE_CURVE ( 'NONE', #13221, #22169, #171, .T. ) ;
#4743=AXIS2_PLACEMENT_3D ( 'NONE', #13130, #18386, #7284 ) ;
#4748=ORIENTED_EDGE ( 'NONE', *, *, #15937, .T. ) ;
#4752=CYLINDRICAL_SURFACE ( 'NONE', #6298, 1.000000000000000888 ) ;
#4757=ORIENTED_EDGE ( 'NONE', *, *, #19144, .T. ) ;
#4761=ORIENTED_EDGE ( 'NONE', *, *, #13853, .F. ) ;
#4764=ORIENTED_EDGE ( 'NONE', *, *, #16506, .F. ) ;
#4768=EDGE_CURVE ( 'NONE', #13833, #5846, #15995, .T. ) ;
#4769=AXIS2_PLACEMENT_3D ( 'NONE', #15579, #15956, #23044 ) ;
#4770=CARTESIAN_POINT ( 'NONE',  ( 33.99999999999998579, -1.387778780781445676E-14, 9.500000000000000000 ) ) ;
#4772=CARTESIAN_POINT ( 'NONE',  ( -21.13207267780287069, 38.32709852940855910, 12.00000000000000000 ) ) ;
#4784=ORIENTED_EDGE ( 'NONE', *, *, #15456, .F. ) ;
#4789=VECTOR ( 'NONE', #5458, 1000.000000000000227 ) ;
#4791=EDGE_CURVE ( 'NONE', #8445, #2607, #14519, .T. ) ;
#4799=EDGE_CURVE ( 'NONE', #10396, #20942, #9874, .T. ) ;
#4812=TOROIDAL_SURFACE ( 'NONE', #22730, 49.00000000000000000, 1.000000000000000000 ) ;
#4815=CIRCLE ( 'NONE', #14518, 1.000000000000000888 ) ;
#4839=TOROIDAL_SURFACE ( 'NONE', #6370, 5.999999999999999112, 1.000000000000000000 ) ;
#4841=CARTESIAN_POINT ( 'NONE',  ( -0.9830802669677229932, 45.00000000000000000, 0.000000000000000000 ) ) ;
#4854=CARTESIAN_POINT ( 'NONE',  ( -29.00000000000000000, 29.49999999999999645, 0.000000000000000000 ) ) ;
#4855=EDGE_CURVE ( 'NONE', #2378, #20352, #24048, .T. ) ;
#4858=EDGE_CURVE ( 'NONE', #6705, #2772, #19675, .T. ) ;
#4870=AXIS2_PLACEMENT_3D ( 'NONE', #618, #2315, #4648 ) ;
#4872=DIRECTION ( 'NONE',  ( -0.000000000000000000, 0.000000000000000000, 1.000000000000000000 ) ) ;
#4885=VERTEX_POINT ( 'NONE', #20623 ) ;
#4887=ADVANCED_FACE ( 'NONE', ( #19042 ), #6333, .F. ) ;
#4898=CARTESIAN_POINT ( 'NONE',  ( 28.27483331787887977, 41.23752903419610760, 0.000000000000000000 ) ) ;
#4899=AXIS2_PLACEMENT_3D ( 'NONE', #18020, #1316, #19383 ) ;
#4904=DIRECTION ( 'NONE',  ( 1.000000000000000000, -0.000000000000000000, 0.000000000000000000 ) ) ;
#4909=DIRECTION ( 'NONE',  ( -0.8757121056631633760, 0.4828336235133056653, 0.000000000000000000 ) ) ;
#4922=VERTEX_POINT ( 'NONE', #12049 ) ;
#4933=ORIENTED_EDGE ( 'NONE', *, *, #7581, .F. ) ;
#4935=EDGE_CURVE ( 'NONE', #7050, #15853, #18866, .T. ) ;
#4943=CARTESIAN_POINT ( 'NONE',  ( 27.70933665152130132, 40.41277845351218190, 11.00000000000000000 ) ) ;
#4949=CARTESIAN_POINT ( 'NONE',  ( -34.00000000000000000, 3.999999999999999112, 9.500000000000000000 ) ) ;
#4979=CARTESIAN_POINT ( 'NONE',  ( -31.10231664966676846, 45.36128193761570770, 12.00000000000000000 ) ) ;
#4983=DIRECTION ( 'NONE',  ( -0.000000000000000000, -0.000000000000000000, -1.000000000000000000 ) ) ;
#4994=DIRECTION ( 'NONE',  ( -0.000000000000000000, -0.000000000000000000, -1.000000000000000000 ) ) ;
#4999=CARTESIAN_POINT ( 'NONE',  ( -21.84999999999999787, 16.67999999999984695, 13.00000000000000178 ) ) ;
#5002=ORIENTED_EDGE ( 'NONE', *, *, #14086, .T. ) ;
#5004=ORIENTED_EDGE ( 'NONE', *, *, #18930, .T. ) ;
#5011=VERTEX_POINT ( 'NONE', #15479 ) ;
#5019=CARTESIAN_POINT ( 'NONE',  ( -29.00000000000000000, -29.49999999999999645, 12.00000000000000000 ) ) ;
#5024=ORIENTED_EDGE ( 'NONE', *, *, #16355, .F. ) ;
#5027=DIRECTION ( 'NONE',  ( 0.000000000000000000, -1.000000000000000000, -0.000000000000000000 ) ) ;
#5033=ORIENTED_EDGE ( 'NONE', *, *, #2996, .T. ) ;
#5039=EDGE_CURVE ( 'NONE', #20363, #18828, #15239, .T. ) ;
#5043=EDGE_CURVE ( 'NONE', #17472, #15489, #22175, .T. ) ;
#5045=ADVANCED_FACE ( 'NONE', ( #21621 ), #17709, .F. ) ;
#5047=ORIENTED_EDGE ( 'NONE', *, *, #15234, .T. ) ;
#5049=CARTESIAN_POINT ( 'NONE',  ( -41.50000000000000000, -28.80990663662250739, 11.00000000000000000 ) ) ;
#5060=AXIS2_PLACEMENT_3D ( 'NONE', #3473, #3117, #10889 ) ;
#5062=CARTESIAN_POINT ( 'NONE',  ( -0.9830802669677229932, 45.00000000000000000, 3.000000000000002665 ) ) ;
#5065=DIRECTION ( 'NONE',  ( 1.000000000000000000, 0.000000000000000000, 0.000000000000000000 ) ) ;
#5069=ORIENTED_EDGE ( 'NONE', *, *, #17306, .F. ) ;
#5083=ORIENTED_EDGE ( 'NONE', *, *, #399, .T. ) ;
#5090=CARTESIAN_POINT ( 'NONE',  ( 41.00000000000000000, 26.23076770084981746, 12.00000000000000000 ) ) ;
#5091=AXIS2_PLACEMENT_3D ( 'NONE', #11856, #21398, #17729 ) ;
#5092=DIRECTION ( 'NONE',  ( 0.000000000000000000, 0.000000000000000000, -1.000000000000000000 ) ) ;
#5100=LINE ( 'NONE', #5348, #23559 ) ;
#5102=DIRECTION ( 'NONE',  ( -0.000000000000000000, -0.000000000000000000, 1.000000000000000000 ) ) ;
#5104=CARTESIAN_POINT ( 'NONE',  ( 29.00000000000000000, -29.50000000000000355, 12.00000000000000000 ) ) ;
#5108=ADVANCED_FACE ( 'NONE', ( #17842 ), #5261, .F. ) ;
#5117=CARTESIAN_POINT ( 'NONE',  ( 20.85000000000000497, 16.67999999999999972, 14.50000000000000000 ) ) ;
#5118=AXIS2_PLACEMENT_3D ( 'NONE', #16372, #14191, #12594 ) ;
#5126=DIRECTION ( 'NONE',  ( 1.000000000000000000, 0.000000000000000000, 0.000000000000000000 ) ) ;
#5132=EDGE_CURVE ( 'NONE', #21270, #2607, #22793, .T. ) ;
#5139=AXIS2_PLACEMENT_3D ( 'NONE', #19269, #4521, #13901 ) ;
#5141=FACE_OUTER_BOUND ( 'NONE', #13926, .T. ) ;
#5144=FACE_OUTER_BOUND ( 'NONE', #21466, .T. ) ;
#5154=ORIENTED_EDGE ( 'NONE', *, *, #11206, .F. ) ;
#5164=EDGE_CURVE ( 'NONE', #21270, #430, #15366, .T. ) ;
#5178=CARTESIAN_POINT ( 'NONE',  ( -39.00000000000000000, 0.000000000000000000, 11.00000000000000000 ) ) ;
#5180=ORIENTED_EDGE ( 'NONE', *, *, #17847, .T. ) ;
#5181=FACE_OUTER_BOUND ( 'NONE', #9786, .T. ) ;
#5184=CARTESIAN_POINT ( 'NONE',  ( 29.00000000000000000, 29.50000000000000355, 11.50000000000000000 ) ) ;
#5185=DIRECTION ( 'NONE',  ( 0.000000000000000000, 0.000000000000000000, -1.000000000000000000 ) ) ;
#5188=DIRECTION ( 'NONE',  ( 1.000000000000000000, 0.000000000000000000, 0.000000000000000000 ) ) ;
#5200=ORIENTED_EDGE ( 'NONE', *, *, #12853, .F. ) ;
#5205=CARTESIAN_POINT ( 'NONE',  ( -30.31394790604173295, -39.41330121100982353, 11.00000000000000000 ) ) ;
#5209=DIRECTION ( 'NONE',  ( -1.000000000000000000, -0.000000000000000000, 0.000000000000000000 ) ) ;
#5216=ORIENTED_EDGE ( 'NONE', *, *, #22673, .T. ) ;
#5218=VERTEX_POINT ( 'NONE', #14645 ) ;
#5244=VECTOR ( 'NONE', #7846, 1000.000000000000000 ) ;
#5261=CYLINDRICAL_SURFACE ( 'NONE', #11453, 4.999999999999997335 ) ;
#5262=ORIENTED_EDGE ( 'NONE', *, *, #22910, .F. ) ;
#5268=DIRECTION ( 'NONE',  ( -0.000000000000000000, -0.000000000000000000, -1.000000000000000000 ) ) ;
#5276=ORIENTED_EDGE ( 'NONE', *, *, #4465, .F. ) ;
#5277=CIRCLE ( 'NONE', #985, 10.00000000000000888 ) ;
#5305=FACE_OUTER_BOUND ( 'NONE', #14551, .T. ) ;
#5321=CARTESIAN_POINT ( 'NONE',  ( -40.00000000000000000, 28.80990663662251450, 0.000000000000000000 ) ) ;
#5338=CARTESIAN_POINT ( 'NONE',  ( -40.77574956473004164, -27.49633847812775755, 12.00000000000000000 ) ) ;
#5339=ADVANCED_FACE ( 'NONE', ( #15270 ), #18973, .T. ) ;
#5344=CARTESIAN_POINT ( 'NONE',  ( 29.00000000000000000, 29.50000000000000355, 11.50000000000000000 ) ) ;
#5348=CARTESIAN_POINT ( 'NONE',  ( -2.983080266967717442, 45.00000000000000000, 3.000000000000002665 ) ) ;
#5351=DIRECTION ( 'NONE',  ( 0.000000000000000000, 0.000000000000000000, 1.000000000000000000 ) ) ;
#5357=ORIENTED_EDGE ( 'NONE', *, *, #20017, .T. ) ;
#5360=DIRECTION ( 'NONE',  ( 1.000000000000000000, 0.000000000000000000, -0.000000000000000000 ) ) ;
#5368=ORIENTED_EDGE ( 'NONE', *, *, #5043, .T. ) ;
#5370=CARTESIAN_POINT ( 'NONE',  ( -29.00000000000000000, -3.851859888774471706E-31, 11.00000000000000000 ) ) ;
#5373=CYLINDRICAL_SURFACE ( 'NONE', #16504, 1.500000000000001332 ) ;
#5387=ORIENTED_EDGE ( 'NONE', *, *, #18930, .F. ) ;
#5394=CIRCLE ( 'NONE', #19037, 1.000000000000000888 ) ;
#5397=ORIENTED_EDGE ( 'NONE', *, *, #12498, .F. ) ;
#5399=DIRECTION ( 'NONE',  ( -0.000000000000000000, -0.000000000000000000, 1.000000000000000000 ) ) ;
#5406=DIRECTION ( 'NONE',  ( 1.000000000000000000, -1.776356839400250465E-15, 0.000000000000000000 ) ) ;
#5427=DIRECTION ( 'NONE',  ( 0.000000000000000000, 0.000000000000000000, -1.000000000000000000 ) ) ;
#5440=EDGE_CURVE ( 'NONE', #3497, #1636, #22394, .T. ) ;
#5454=ORIENTED_EDGE ( 'NONE', *, *, #9462, .F. ) ;
#5458=DIRECTION ( 'NONE',  ( -0.8757121056631640421, 0.4828336235133042775, -0.000000000000000000 ) ) ;
#5463=EDGE_CURVE ( 'NONE', #11221, #5671, #14962, .T. ) ;
#5475=AXIS2_PLACEMENT_3D ( 'NONE', #7932, #10005, #11841 ) ;
#5494=EDGE_LOOP ( 'NONE', ( #9504, #21215, #4764, #10518 ) ) ;
#5504=EDGE_CURVE ( 'NONE', #21975, #8445, #15409, .T. ) ;
#5505=ORIENTED_EDGE ( 'NONE', *, *, #17891, .T. ) ;
#5506=DIRECTION ( 'NONE',  ( 0.000000000000000000, -0.000000000000000000, -1.000000000000000000 ) ) ;
#5519=VECTOR ( 'NONE', #12743, 1000.000000000000000 ) ;
#5531=EDGE_CURVE ( 'NONE', #16881, #7962, #12095, .T. ) ;
#5535=CARTESIAN_POINT ( 'NONE',  ( -37.00000000000000711, -29.49999999999999645, 11.50000000000000000 ) ) ;
#5539=DIRECTION ( 'NONE',  ( 0.000000000000000000, -0.000000000000000000, -1.000000000000000000 ) ) ;
#5559=AXIS2_PLACEMENT_3D ( 'NONE', #10619, #922, #19466 ) ;
#5563=DIRECTION ( 'NONE',  ( 0.000000000000000000, 0.000000000000000000, 1.000000000000000000 ) ) ;
#5568=ORIENTED_EDGE ( 'NONE', *, *, #12758, .T. ) ;
#5569=VECTOR ( 'NONE', #4719, 1000.000000000000000 ) ;
#5602=FACE_OUTER_BOUND ( 'NONE', #1101, .T. ) ;
#5608=EDGE_CURVE ( 'NONE', #666, #19209, #20923, .T. ) ;
#5615=FACE_OUTER_BOUND ( 'NONE', #10528, .T. ) ;
#5634=AXIS2_PLACEMENT_3D ( 'NONE', #18608, #2245, #20562 ) ;
#5653=DIRECTION ( 'NONE',  ( -0.000000000000000000, 0.000000000000000000, 1.000000000000000000 ) ) ;
#5654=ORIENTED_EDGE ( 'NONE', *, *, #19047, .F. ) ;
#5656=CIRCLE ( 'NONE', #7559, 1.000000000000000888 ) ;
#5670=CARTESIAN_POINT ( 'NONE',  ( 20.99999999999999645, 29.50000000000000355, 11.50000000000000000 ) ) ;
#5671=VERTEX_POINT ( 'NONE', #6886 ) ;
#5678=ORIENTED_EDGE ( 'NONE', *, *, #2126, .T. ) ;
#5684=ORIENTED_EDGE ( 'NONE', *, *, #15911, .T. ) ;
#5698=AXIS2_PLACEMENT_3D ( 'NONE', #16092, #10478, #3162 ) ;
#5701=CYLINDRICAL_SURFACE ( 'NONE', #17784, 1.000000000000000000 ) ;
#5702=FACE_BOUND ( 'NONE', #8465, .T. ) ;
#5707=CIRCLE ( 'NONE', #22462, 2.024999999999999911 ) ;
#5708=DIRECTION ( 'NONE',  ( 0.000000000000000000, 1.000000000000000000, -0.000000000000000000 ) ) ;
#5710=ORIENTED_EDGE ( 'NONE', *, *, #5164, .T. ) ;
#5712=CARTESIAN_POINT ( 'NONE',  ( 33.99999999999998579, 3.999999999999985345, 9.500000000000000000 ) ) ;
#5714=FACE_OUTER_BOUND ( 'NONE', #21852, .T. ) ;
#5719=ORIENTED_EDGE ( 'NONE', *, *, #19028, .F. ) ;
#5720=VERTEX_POINT ( 'NONE', #17867 ) ;
#5721=ORIENTED_EDGE ( 'NONE', *, *, #21560, .F. ) ;
#5730=CARTESIAN_POINT ( 'NONE',  ( 21.13207267780287069, -38.32709852940855910, 0.000000000000000000 ) ) ;
#5733=DIRECTION ( 'NONE',  ( -1.000000000000000000, 0.000000000000000000, 0.000000000000000000 ) ) ;
#5734=DIRECTION ( 'NONE',  ( 0.000000000000000000, 0.000000000000000000, 1.000000000000000000 ) ) ;
#5736=APPLICATION_CONTEXT ( 'automotive_design' ) ;
#5738=ORIENTED_EDGE ( 'NONE', *, *, #23440, .F. ) ;
#5744=ORIENTED_EDGE ( 'NONE', *, *, #17301, .F. ) ;
#5752=DIRECTION ( 'NONE',  ( -0.000000000000000000, -0.000000000000000000, 1.000000000000000000 ) ) ;
#5771=CARTESIAN_POINT ( 'NONE',  ( 40.29291594121673370, 26.62062637246459218, 11.00000000000000000 ) ) ;
#5775=ADVANCED_FACE ( 'NONE', ( #10866 ), #19637, .T. ) ;
#5782=ORIENTED_EDGE ( 'NONE', *, *, #19600, .T. ) ;
#5786=CARTESIAN_POINT ( 'NONE',  ( -0.9830802669677241035, 45.00000000000000000, 4.201721238055123209 ) ) ;
#5787=FACE_OUTER_BOUND ( 'NONE', #23488, .T. ) ;
#5800=ORIENTED_EDGE ( 'NONE', *, *, #14707, .T. ) ;
#5806=LINE ( 'NONE', #2014, #18171 ) ;
#5818=EDGE_CURVE ( 'NONE', #11492, #20529, #14928, .T. ) ;
#5826=VERTEX_POINT ( 'NONE', #16972 ) ;
#5838=ORIENTED_EDGE ( 'NONE', *, *, #5818, .F. ) ;
#5840=EDGE_CURVE ( 'NONE', #13339, #21886, #11811, .T. ) ;
#5846=VERTEX_POINT ( 'NONE', #9382 ) ;
#5853=ORIENTED_EDGE ( 'NONE', *, *, #8242, .F. ) ;
#5855=DIRECTION ( 'NONE',  ( 0.000000000000000000, 0.000000000000000000, 1.000000000000000000 ) ) ;
#5857=PLANE ( 'NONE',  #23228 ) ;
#5865=DIRECTION ( 'NONE',  ( -0.000000000000000000, -1.000000000000000000, -0.000000000000000000 ) ) ;
#5873=ORIENTED_EDGE ( 'NONE', *, *, #18435, .T. ) ;
#5877=FACE_OUTER_BOUND ( 'NONE', #3632, .T. ) ;
#5879=AXIS2_PLACEMENT_3D ( 'NONE', #4979, #945, #12389 ) ;
#5883=ORIENTED_EDGE ( 'NONE', *, *, #11948, .F. ) ;
#5887=CARTESIAN_POINT ( 'NONE',  ( -28.27483331787888687, 41.23752903419610050, 12.00000000000000000 ) ) ;
#5890=FACE_OUTER_BOUND ( 'NONE', #16010, .T. ) ;
#5897=DIRECTION ( 'NONE',  ( 1.000000000000000000, 0.000000000000000000, -0.000000000000000000 ) ) ;
#5905=CARTESIAN_POINT ( 'NONE',  ( 29.00000000000000000, -29.50000000000000355, 12.00000000000000000 ) ) ;
#5906=ORIENTED_EDGE ( 'NONE', *, *, #8251, .F. ) ;
#5912=VERTEX_POINT ( 'NONE', #2093 ) ;
#5919=ORIENTED_EDGE ( 'NONE', *, *, #11874, .F. ) ;
#5920=CARTESIAN_POINT ( 'NONE',  ( -41.00000000000000000, -26.23076770084981746, 12.00000000000000000 ) ) ;
#5929=EDGE_CURVE ( 'NONE', #13005, #15853, #919, .T. ) ;
#5940=CIRCLE ( 'NONE', #11748, 1.000000000000000888 ) ;
#5957=AXIS2_PLACEMENT_3D ( 'NONE', #11318, #18796, #2443 ) ;
#5960=PLANE ( 'NONE',  #98 ) ;
#5963=EDGE_CURVE ( 'NONE', #145, #13833, #21916, .T. ) ;
#5965=EDGE_CURVE ( 'NONE', #17123, #13005, #3208, .T. ) ;
#5973=CIRCLE ( 'NONE', #6746, 1.000000000000000888 ) ;
#5978=CARTESIAN_POINT ( 'NONE',  ( 0.000000000000000000, 0.000000000000000000, 0.000000000000000000 ) ) ;
#5981=DIRECTION ( 'NONE',  ( 0.000000000000000000, 1.000000000000000000, 3.469446951953610639E-15 ) ) ;
#5982=DIRECTION ( 'NONE',  ( -1.000000000000000000, 2.600433232233976523E-16, -0.000000000000000000 ) ) ;
#6000=CARTESIAN_POINT ( 'NONE',  ( 29.00000000000000000, -29.50000000000000355, 12.00000000000000000 ) ) ;
#6015=ADVANCED_FACE ( 'NONE', ( #5787 ), #7257, .F. ) ;
#6018=AXIS2_PLACEMENT_3D ( 'NONE', #3613, #22180, #22534 ) ;
#6028=AXIS2_PLACEMENT_3D ( 'NONE', #22512, #20430, #9553 ) ;
#6034=TOROIDAL_SURFACE ( 'NONE', #4489, 10.00000000000000888, 1.000000000000000000 ) ;
#6044=ORIENTED_EDGE ( 'NONE', *, *, #7448, .F. ) ;
#6047=CARTESIAN_POINT ( 'NONE',  ( 31.10231664966676846, -45.36128193761570770, 12.00000000000000000 ) ) ;
#6050=EDGE_CURVE ( 'NONE', #411, #18498, #5940, .T. ) ;
#6061=ORIENTED_EDGE ( 'NONE', *, *, #19924, .F. ) ;
#6068=ORIENTED_EDGE ( 'NONE', *, *, #9030, .T. ) ;
#6074=LINE ( 'NONE', #19123, #19046 ) ;
#6079=VECTOR ( 'NONE', #14699, 1000.000000000000000 ) ;
#6081=VECTOR ( 'NONE', #9309, 1000.000000000000000 ) ;
#6086=LINE ( 'NONE', #2300, #487 ) ;
#6090=DIRECTION ( 'NONE',  ( 1.000000000000000000, 0.000000000000000000, 0.000000000000000000 ) ) ;
#6103=DIRECTION ( 'NONE',  ( 1.000000000000000000, 0.000000000000000000, 0.000000000000000000 ) ) ;
#6131=ADVANCED_FACE ( 'NONE', ( #21147, #4204, #13464, #11615, #11494, #15780, #11863 ), #17597, .F. ) ;
#6132=DIRECTION ( 'NONE',  ( -0.000000000000000000, -0.000000000000000000, -1.000000000000000000 ) ) ;
#6149=ORIENTED_EDGE ( 'NONE', *, *, #13476, .F. ) ;
#6153=EDGE_CURVE ( 'NONE', #11221, #13932, #7862, .T. ) ;
#6154=CARTESIAN_POINT ( 'NONE',  ( 29.00000000000000000, 29.50000000000000355, 12.00000000000000000 ) ) ;
#6156=AXIS2_PLACEMENT_3D ( 'NONE', #14719, #5209, #5092 ) ;
#6161=ORIENTED_EDGE ( 'NONE', *, *, #19982, .F. ) ;
#6167=CARTESIAN_POINT ( 'NONE',  ( 41.50000000000000000, -28.80990663662250739, 12.00000000000000000 ) ) ;
#6170=DIRECTION ( 'NONE',  ( -0.000000000000000000, 1.000000000000000000, 0.000000000000000000 ) ) ;
#6179=EDGE_LOOP ( 'NONE', ( #5004, #18699, #22611, #21546 ) ) ;
#6182=EDGE_CURVE ( 'NONE', #21802, #13005, #492, .T. ) ;
#6183=DIRECTION ( 'NONE',  ( -0.000000000000000000, -0.000000000000000000, -1.000000000000000000 ) ) ;
#6212=ADVANCED_FACE ( 'NONE', ( #21404 ), #6986, .F. ) ;
#6231=DIRECTION ( 'NONE',  ( -0.000000000000000000, -0.000000000000000000, -1.000000000000000000 ) ) ;
#6239=ORIENTED_EDGE ( 'NONE', *, *, #3474, .F. ) ;
#6246=ORIENTED_EDGE ( 'NONE', *, *, #12525, .F. ) ;
#6248=EDGE_CURVE ( 'NONE', #14909, #5671, #7464, .T. ) ;
#6250=ORIENTED_EDGE ( 'NONE', *, *, #6677, .F. ) ;
#6253=ORIENTED_EDGE ( 'NONE', *, *, #20841, .F. ) ;
#6268=ORIENTED_EDGE ( 'NONE', *, *, #4520, .F. ) ;
#6279=DIRECTION ( 'NONE',  ( 0.000000000000000000, 0.000000000000000000, 1.000000000000000000 ) ) ;
#6294=ORIENTED_EDGE ( 'NONE', *, *, #17541, .T. ) ;
#6298=AXIS2_PLACEMENT_3D ( 'NONE', #21216, #1208, #11925 ) ;
#6311=ORIENTED_EDGE ( 'NONE', *, *, #6436, .F. ) ;
#6318=CIRCLE ( 'NONE', #1658, 8.000000000000003553 ) ;
#6321=CARTESIAN_POINT ( 'NONE',  ( 40.00000000000000000, 0.000000000000000000, 0.000000000000000000 ) ) ;
#6332=ORIENTED_EDGE ( 'NONE', *, *, #1464, .T. ) ;
#6333=PLANE ( 'NONE',  #4870 ) ;
#6339=DIRECTION ( 'NONE',  ( 1.000000000000000000, 0.000000000000000000, 0.000000000000000000 ) ) ;
#6340=AXIS2_PLACEMENT_3D ( 'NONE', #14743, #22206, #7186 ) ;
#6346=EDGE_CURVE ( 'NONE', #2739, #23101, #1961, .T. ) ;
#6347=ADVANCED_FACE ( 'NONE', ( #18582 ), #16618, .F. ) ;
#6352=ORIENTED_EDGE ( 'NONE', *, *, #12398, .F. ) ;
#6353=FACE_OUTER_BOUND ( 'NONE', #22655, .T. ) ;
#6355=CARTESIAN_POINT ( 'NONE',  ( 40.77574956473004164, -27.49633847812775755, 11.00000000000000000 ) ) ;
#6356=( NAMED_UNIT ( * ) SI_UNIT ( $, .STERADIAN. ) SOLID_ANGLE_UNIT ( ) );
#6370=AXIS2_PLACEMENT_3D ( 'NONE', #17189, #17443, #623 ) ;
#6375=EDGE_LOOP ( 'NONE', ( #17037, #23118 ) ) ;
#6385=EDGE_LOOP ( 'NONE', ( #22774, #15050, #23273, #10952 ) ) ;
#6388=CIRCLE ( 'NONE', #156, 1.500000000000001332 ) ;
#6389=FACE_BOUND ( 'NONE', #22028, .T. ) ;
#6396=CARTESIAN_POINT ( 'NONE',  ( 41.00000000000000000, -5.000000000000015099, 9.500000000000000000 ) ) ;
#6407=AXIS2_PLACEMENT_3D ( 'NONE', #8928, #9050, #16368 ) ;
#6408=ORIENTED_EDGE ( 'NONE', *, *, #18251, .F. ) ;
#6415=ADVANCED_FACE ( 'NONE', ( #18804 ), #9280, .T. ) ;
#6417=FACE_OUTER_BOUND ( 'NONE', #12658, .T. ) ;
#6418=ORIENTED_EDGE ( 'NONE', *, *, #21397, .F. ) ;
#6436=EDGE_CURVE ( 'NONE', #5218, #1117, #4815, .T. ) ;
#6438=CARTESIAN_POINT ( 'NONE',  ( -19.84999999999999787, -16.67999999999985761, 13.50000000000000178 ) ) ;
#6451=DIRECTION ( 'NONE',  ( -1.000000000000000000, 0.000000000000000000, 0.000000000000000000 ) ) ;
#6452=DIRECTION ( 'NONE',  ( 1.000000000000000000, 0.000000000000000000, 0.000000000000000000 ) ) ;
#6457=DIRECTION ( 'NONE',  ( 0.5654966663575753394, -0.8247505806839234843, 0.000000000000000000 ) ) ;
#6460=DIRECTION ( 'NONE',  ( -0.000000000000000000, -0.000000000000000000, -1.000000000000000000 ) ) ;
#6464=ORIENTED_EDGE ( 'NONE', *, *, #20894, .F. ) ;
#6470=EDGE_CURVE ( 'NONE', #430, #4506, #22133, .T. ) ;
#6479=CARTESIAN_POINT ( 'NONE',  ( 33.99999999999998579, -1.387778780781445676E-14, 10.49999999999999822 ) ) ;
#6488=CYLINDRICAL_SURFACE ( 'NONE', #17637, 8.000000000000003553 ) ;
#6489=DIRECTION ( 'NONE',  ( 1.000000000000000000, 2.600433232233976523E-16, 0.000000000000000000 ) ) ;
#6490=AXIS2_PLACEMENT_3D ( 'NONE', #10847, #13541, #9490 ) ;
#6494=FACE_OUTER_BOUND ( 'NONE', #21879, .T. ) ;
#6495=CARTESIAN_POINT ( 'NONE',  ( -1.999999999999994449, -45.00000000000000000, 3.000000000000002665 ) ) ;
#6500=DIRECTION ( 'NONE',  ( -0.000000000000000000, 0.000000000000000000, 1.000000000000000000 ) ) ;
#6511=ORIENTED_EDGE ( 'NONE', *, *, #19154, .F. ) ;
#6512=CARTESIAN_POINT ( 'NONE',  ( 40.00000000000000000, -29.49999999999999645, 0.000000000000000000 ) ) ;
#6520=ORIENTED_EDGE ( 'NONE', *, *, #11367, .T. ) ;
#6521=DIRECTION ( 'NONE',  ( 1.000000000000000000, 0.000000000000000000, 0.000000000000000000 ) ) ;
#6523=DIRECTION ( 'NONE',  ( 1.000000000000000000, 0.000000000000000000, 0.000000000000000000 ) ) ;
#6526=EDGE_LOOP ( 'NONE', ( #4621, #6804, #24017, #3769 ) ) ;
#6528=FACE_OUTER_BOUND ( 'NONE', #13209, .T. ) ;
#6539=CARTESIAN_POINT ( 'NONE',  ( 41.00000000000000000, 26.23076770084981746, 12.00000000000000000 ) ) ;
#6541=DIRECTION ( 'NONE',  ( 3.469446951953610639E-15, -1.000000000000000000, 0.000000000000000000 ) ) ;
#6559=DIRECTION ( 'NONE',  ( -0.000000000000000000, 1.000000000000000000, -0.000000000000000000 ) ) ;
#6568=DIRECTION ( 'NONE',  ( 0.000000000000000000, -0.000000000000000000, -1.000000000000000000 ) ) ;
#6573=CARTESIAN_POINT ( 'NONE',  ( -34.00000000000000000, -3.851859888774471706E-31, 11.00000000000000000 ) ) ;
#6575=ORIENTED_EDGE ( 'NONE', *, *, #5440, .T. ) ;
#6577=LINE ( 'NONE', #14354, #23095 ) ;
#6578=EDGE_CURVE ( 'NONE', #15489, #9530, #15376, .T. ) ;
#6583=CARTESIAN_POINT ( 'NONE',  ( -42.00000000000000000, 0.000000000000000000, 12.00000000000000000 ) ) ;
#6584=CARTESIAN_POINT ( 'NONE',  ( -30.44534269664590553, -40.40463133211081015, 12.00000000000000000 ) ) ;
#6601=DIRECTION ( 'NONE',  ( 0.000000000000000000, 0.000000000000000000, -1.000000000000000000 ) ) ;
#6617=FACE_OUTER_BOUND ( 'NONE', #23425, .T. ) ;
#6620=ORIENTED_EDGE ( 'NONE', *, *, #10122, .F. ) ;
#6625=DIRECTION ( 'NONE',  ( 0.000000000000000000, 0.000000000000000000, 1.000000000000000000 ) ) ;
#6629=VECTOR ( 'NONE', #1180, 1000.000000000000000 ) ;
#6634=DIRECTION ( 'NONE',  ( 0.8757121056631640421, 0.4828336235133042775, -0.000000000000000000 ) ) ;
#6635=ORIENTED_EDGE ( 'NONE', *, *, #1717, .F. ) ;
#6639=CARTESIAN_POINT ( 'NONE',  ( 39.00000000000000000, 0.000000000000000000, 11.00000000000000000 ) ) ;
#6648=EDGE_CURVE ( 'NONE', #13339, #12632, #8666, .T. ) ;
#6653=FACE_OUTER_BOUND ( 'NONE', #20812, .T. ) ;
#6655=DIRECTION ( 'NONE',  ( -0.000000000000000000, 1.000000000000000000, -0.000000000000000000 ) ) ;
#6656=FACE_OUTER_BOUND ( 'NONE', #9787, .T. ) ;
#6666=DIRECTION ( 'NONE',  ( -1.000000000000000000, 0.000000000000000000, 0.000000000000000000 ) ) ;
#6667=CARTESIAN_POINT ( 'NONE',  ( 0.000000000000000000, -45.00000000000000000, 3.000000000000002665 ) ) ;
#6669=DIRECTION ( 'NONE',  ( -0.000000000000000000, 0.000000000000000000, 1.000000000000000000 ) ) ;
#6677=EDGE_CURVE ( 'NONE', #1409, #2972, #13934, .T. ) ;
#6705=VERTEX_POINT ( 'NONE', #10700 ) ;
#6707=ADVANCED_FACE ( 'NONE', ( #10575 ), #19875, .T. ) ;
#6709=CARTESIAN_POINT ( 'NONE',  ( -40.00000000000000000, 29.49999999999999645, 12.00000000000000000 ) ) ;
#6714=DIRECTION ( 'NONE',  ( -1.000000000000000000, 0.000000000000000000, 0.000000000000000000 ) ) ;
#6715=EDGE_CURVE ( 'NONE', #11167, #16259, #22191, .T. ) ;
#6738=ADVANCED_FACE ( 'NONE', ( #6494 ), #23102, .T. ) ;
#6741=EDGE_CURVE ( 'NONE', #14736, #4131, #3627, .T. ) ;
#6746=AXIS2_PLACEMENT_3D ( 'NONE', #3011, #21180, #23501 ) ;
#6752=DIRECTION ( 'NONE',  ( -0.000000000000000000, 0.000000000000000000, 1.000000000000000000 ) ) ;
#6753=CIRCLE ( 'NONE', #5559, 1.999999999999994449 ) ;
#6754=DIRECTION ( 'NONE',  ( 0.000000000000000000, -0.000000000000000000, -1.000000000000000000 ) ) ;
#6758=DIRECTION ( 'NONE',  ( 1.000000000000000000, 0.000000000000000000, 0.000000000000000000 ) ) ;
#6769=CONICAL_SURFACE ( 'NONE', #13762, 1.999999999999994449, 1.029744258676653201 ) ;
#6770=AXIS2_PLACEMENT_3D ( 'NONE', #8711, #16160, #1418 ) ;
#6774=DIRECTION ( 'NONE',  ( -0.000000000000000000, -0.000000000000000000, 1.000000000000000000 ) ) ;
#6780=LINE ( 'NONE', #16039, #5569 ) ;
#6799=EDGE_CURVE ( 'NONE', #21725, #21270, #7170, .T. ) ;
#6804=ORIENTED_EDGE ( 'NONE', *, *, #13715, .F. ) ;
#6807=AXIS2_PLACEMENT_3D ( 'NONE', #17147, #446, #15444 ) ;
#6810=CARTESIAN_POINT ( 'NONE',  ( -34.00000000000000000, -3.851859888774471706E-31, 11.00000000000000000 ) ) ;
#6812=VECTOR ( 'NONE', #8811, 1000.000000000000000 ) ;
#6813=ORIENTED_EDGE ( 'NONE', *, *, #6182, .T. ) ;
#6816=DIRECTION ( 'NONE',  ( 1.000000000000000000, 0.000000000000000000, 0.000000000000000000 ) ) ;
#6826=EDGE_CURVE ( 'NONE', #19949, #5846, #12962, .T. ) ;
#6835=CARTESIAN_POINT ( 'NONE',  ( 30.44534269664590553, -40.40463133211081015, 0.000000000000000000 ) ) ;
#6842=DIRECTION ( 'NONE',  ( 0.000000000000000000, 0.000000000000000000, -1.000000000000000000 ) ) ;
#6847=VECTOR ( 'NONE', #22608, 1000.000000000000000 ) ;
#6848=DIRECTION ( 'NONE',  ( 0.000000000000000000, 0.000000000000000000, -1.000000000000000000 ) ) ;
#6854=CIRCLE ( 'NONE', #13852, 4.999999999999997335 ) ;
#6859=ORIENTED_EDGE ( 'NONE', *, *, #2126, .F. ) ;
#6875=LINE ( 'NONE', #20171, #6812 ) ;
#6881=VECTOR ( 'NONE', #16414, 1000.000000000000000 ) ;
#6886=CARTESIAN_POINT ( 'NONE',  ( -30.44534269664590553, 40.40463133211079594, 11.00000000000000000 ) ) ;
#6890=CARTESIAN_POINT ( 'NONE',  ( 41.00000000000000000, 4.999999999999986677, 9.500000000000000000 ) ) ;
#6894=VERTEX_POINT ( 'NONE', #18639 ) ;
#6913=CARTESIAN_POINT ( 'NONE',  ( 42.00000000000000000, 5.999999999999986677, 12.00000000000000000 ) ) ;
#6920=CARTESIAN_POINT ( 'NONE',  ( -21.84999999999999787, -16.67999999999984340, 12.00000000000000000 ) ) ;
#6923=CYLINDRICAL_SURFACE ( 'NONE', #4098, 1.999999999999994449 ) ;
#6926=EDGE_CURVE ( 'NONE', #4459, #12416, #15310, .T. ) ;
#6928=CARTESIAN_POINT ( 'NONE',  ( 41.51716637648670627, -25.94562225875360895, 12.00000000000000000 ) ) ;
#6930=DIRECTION ( 'NONE',  ( -0.000000000000000000, 0.000000000000000000, 1.000000000000000000 ) ) ;
#6932=FACE_OUTER_BOUND ( 'NONE', #22888, .T. ) ;
#6933=EDGE_CURVE ( 'NONE', #12069, #3762, #2455, .T. ) ;
#6941=CARTESIAN_POINT ( 'NONE',  ( 2.454813078130514813E-15, -16.67999999999999972, 13.50000000000000178 ) ) ;
#6943=CARTESIAN_POINT ( 'NONE',  ( -37.00000000000000711, -29.49999999999999645, 11.50000000000000000 ) ) ;
#6960=ADVANCED_FACE ( 'NONE', ( #14220 ), #6769, .F. ) ;
#6962=FACE_BOUND ( 'NONE', #13085, .T. ) ;
#6971=CARTESIAN_POINT ( 'NONE',  ( -34.00000000000000000, -3.851859888774471706E-31, 9.500000000000000000 ) ) ;
#6986=CYLINDRICAL_SURFACE ( 'NONE', #10593, 4.999999999999997335 ) ;
#6996=AXIS2_PLACEMENT_3D ( 'NONE', #9514, #6231, #21001 ) ;
#6997=ADVANCED_FACE ( 'NONE', ( #12745 ), #20206, .F. ) ;
#7005=EDGE_CURVE ( 'NONE', #2972, #23101, #8727, .T. ) ;
#7015=DIRECTION ( 'NONE',  ( 1.000000000000000000, 2.600433232233976523E-16, -0.000000000000000000 ) ) ;
#7032=DIRECTION ( 'NONE',  ( 0.000000000000000000, 0.000000000000000000, -1.000000000000000000 ) ) ;
#7040=CARTESIAN_POINT ( 'NONE',  ( 33.99999999999998579, 3.999999999999985345, 9.500000000000000000 ) ) ;
#7042=CARTESIAN_POINT ( 'NONE',  ( -34.00000000000000000, 5.999999999999999112, 11.00000000000000000 ) ) ;
#7044=LINE ( 'NONE', #3399, #22620 ) ;
#7045=EDGE_LOOP ( 'NONE', ( #4933, #7112, #17015, #12718 ) ) ;
#7050=VERTEX_POINT ( 'NONE', #11362 ) ;
#7064=LINE ( 'NONE', #18069, #19234 ) ;
#7065=AXIS2_PLACEMENT_3D ( 'NONE', #2755, #12264, #6666 ) ;
#7067=CARTESIAN_POINT ( 'NONE',  ( 19.85000000000000142, -16.67999999999999616, 14.50000000000000000 ) ) ;
#7074=DIRECTION ( 'NONE',  ( -0.000000000000000000, -0.000000000000000000, -1.000000000000000000 ) ) ;
#7075=CARTESIAN_POINT ( 'NONE',  ( 40.77574956473004164, 27.49633847812775755, 11.00000000000000000 ) ) ;
#7083=DIRECTION ( 'NONE',  ( -0.000000000000000000, -0.000000000000000000, -1.000000000000000000 ) ) ;
#7085=EDGE_CURVE ( 'NONE', #2102, #3810, #16860, .T. ) ;
#7088=DIRECTION ( 'NONE',  ( 0.000000000000000000, 0.000000000000000000, 1.000000000000000000 ) ) ;
#7091=EDGE_LOOP ( 'NONE', ( #9721, #7557, #20030, #10639 ) ) ;
#7112=ORIENTED_EDGE ( 'NONE', *, *, #19459, .T. ) ;
#7114=ORIENTED_EDGE ( 'NONE', *, *, #4520, .T. ) ;
#7128=FACE_OUTER_BOUND ( 'NONE', #2299, .T. ) ;
#7130=LINE ( 'NONE', #21901, #23080 ) ;
#7133=EDGE_CURVE ( 'NONE', #11854, #19436, #9856, .T. ) ;
#7134=DIRECTION ( 'NONE',  ( -1.000000000000000000, 0.000000000000000000, 0.000000000000000000 ) ) ;
#7135=VECTOR ( 'NONE', #19396, 1000.000000000000000 ) ;
#7139=ORIENTED_EDGE ( 'NONE', *, *, #20776, .F. ) ;
#7144=AXIS2_PLACEMENT_3D ( 'NONE', #2937, #12314, #23560 ) ;
#7152=FACE_OUTER_BOUND ( 'NONE', #20387, .T. ) ;
#7155=VECTOR ( 'NONE', #8467, 1000.000000000000000 ) ;
#7159=EDGE_CURVE ( 'NONE', #8434, #145, #11011, .T. ) ;
#7160=ORIENTED_EDGE ( 'NONE', *, *, #684, .T. ) ;
#7170=LINE ( 'NONE', #22074, #12581 ) ;
#7171=DIRECTION ( 'NONE',  ( -0.000000000000000000, -0.000000000000000000, -1.000000000000000000 ) ) ;
#7179=AXIS2_PLACEMENT_3D ( 'NONE', #13413, #10221, #737 ) ;
#7181=CARTESIAN_POINT ( 'NONE',  ( -40.00000000000000000, -28.80990663662251450, 11.00000000000000000 ) ) ;
#7184=VECTOR ( 'NONE', #20689, 1000.000000000000000 ) ;
#7186=DIRECTION ( 'NONE',  ( 0.000000000000000000, 0.000000000000000000, -1.000000000000000000 ) ) ;
#7190=DIRECTION ( 'NONE',  ( 0.000000000000000000, 1.000000000000000000, 0.000000000000000000 ) ) ;
#7194=CIRCLE ( 'NONE', #19289, 1.000000000000000888 ) ;
#7203=LINE ( 'NONE', #12690, #1684 ) ;
#7213=EDGE_CURVE ( 'NONE', #9993, #12069, #3953, .T. ) ;
#7233=CARTESIAN_POINT ( 'NONE',  ( -29.00000000000000000, -29.49999999999999645, 0.000000000000000000 ) ) ;
#7236=VECTOR ( 'NONE', #20008, 1000.000000000000000 ) ;
#7241=VERTEX_POINT ( 'NONE', #4324 ) ;
#7242=AXIS2_PLACEMENT_3D ( 'NONE', #6154, #21037, #11363 ) ;
#7245=CARTESIAN_POINT ( 'NONE',  ( 41.50000000000000000, 28.80990663662250739, 11.00000000000000000 ) ) ;
#7250=ORIENTED_EDGE ( 'NONE', *, *, #23660, .T. ) ;
#7254=FACE_OUTER_BOUND ( 'NONE', #10883, .T. ) ;
#7257=CYLINDRICAL_SURFACE ( 'NONE', #2085, 1.999999999999994449 ) ;
#7259=ORIENTED_EDGE ( 'NONE', *, *, #13323, .T. ) ;
#7261=CARTESIAN_POINT ( 'NONE',  ( -42.00000000000000711, 26.82133436441678498, 12.00000000000000000 ) ) ;
#7263=ORIENTED_EDGE ( 'NONE', *, *, #18054, .F. ) ;
#7284=DIRECTION ( 'NONE',  ( 0.000000000000000000, 0.000000000000000000, -1.000000000000000000 ) ) ;
#7285=CARTESIAN_POINT ( 'NONE',  ( -42.00000000000000711, 26.82133436441678498, 11.00000000000000000 ) ) ;
#7301=CARTESIAN_POINT ( 'NONE',  ( 34.10000000000000142, 29.50000000000000355, 11.50000000000000000 ) ) ;
#7308=LINE ( 'NONE', #23041, #9532 ) ;
#7328=TOROIDAL_SURFACE ( 'NONE', #18247, 10.00000000000000888, 1.000000000000000000 ) ;
#7339=CARTESIAN_POINT ( 'NONE',  ( 0.000000000000000000, 0.000000000000000000, 0.000000000000000000 ) ) ;
#7344=ORIENTED_EDGE ( 'NONE', *, *, #3459, .T. ) ;
#7351=EDGE_LOOP ( 'NONE', ( #12043, #10402, #794, #137 ) ) ;
#7354=EDGE_CURVE ( 'NONE', #8169, #24045, #13841, .T. ) ;
#7358=DIRECTION ( 'NONE',  ( 0.4828336235133057208, -0.8757121056631633760, 0.000000000000000000 ) ) ;
#7361=LINE ( 'NONE', #21900, #5519 ) ;
#7364=DIRECTION ( 'NONE',  ( -1.000000000000000000, 2.600433232233976523E-16, 0.000000000000000000 ) ) ;
#7366=CARTESIAN_POINT ( 'NONE',  ( -28.27483331787888687, 41.23752903419610050, 0.000000000000000000 ) ) ;
#7371=ORIENTED_EDGE ( 'NONE', *, *, #2298, .T. ) ;
#7384=CARTESIAN_POINT ( 'NONE',  ( 42.00000000000000000, 5.999999999999986677, 11.00000000000000000 ) ) ;
#7385=VERTEX_POINT ( 'NONE', #19826 ) ;
#7386=CARTESIAN_POINT ( 'NONE',  ( -39.00000000000000711, -29.49999999999999645, 11.00000000000000000 ) ) ;
#7406=LINE ( 'NONE', #115, #11486 ) ;
#7409=CARTESIAN_POINT ( 'NONE',  ( -29.00000000000000000, -29.49999999999999645, 11.50000000000000000 ) ) ;
#7410=DIRECTION ( 'NONE',  ( -1.000000000000000000, 0.000000000000000000, 0.000000000000000000 ) ) ;
#7421=CARTESIAN_POINT ( 'NONE',  ( 29.00000000000000000, 29.50000000000000355, 11.00000000000000000 ) ) ;
#7427=EDGE_CURVE ( 'NONE', #3246, #7598, #1405, .T. ) ;
#7429=CARTESIAN_POINT ( 'NONE',  ( -41.00000000000000000, -6.000000000000000888, 11.00000000000000000 ) ) ;
#7435=ORIENTED_EDGE ( 'NONE', *, *, #10244, .T. ) ;
#7448=EDGE_CURVE ( 'NONE', #20529, #19325, #21881, .T. ) ;
#7462=EDGE_LOOP ( 'NONE', ( #9457, #10021, #6464, #9312 ) ) ;
#7464=CIRCLE ( 'NONE', #16885, 11.00000000000001066 ) ;
#7473=ORIENTED_EDGE ( 'NONE', *, *, #12163, .T. ) ;
#7475=ORIENTED_EDGE ( 'NONE', *, *, #11379, .T. ) ;
#7482=ORIENTED_EDGE ( 'NONE', *, *, #5608, .T. ) ;
#7489=CARTESIAN_POINT ( 'NONE',  ( 33.99999999999998579, -4.000000000000013323, 10.49999999999999822 ) ) ;
#7495=VERTEX_POINT ( 'NONE', #1044 ) ;
#7498=DIRECTION ( 'NONE',  ( 0.000000000000000000, 0.000000000000000000, 1.000000000000000000 ) ) ;
#7506=ADVANCED_FACE ( 'NONE', ( #17870 ), #10209, .T. ) ;
#7507=DIRECTION ( 'NONE',  ( -0.000000000000000000, -0.000000000000000000, -1.000000000000000000 ) ) ;
#7523=DIRECTION ( 'NONE',  ( -1.000000000000000000, -2.600433232233976523E-16, -0.000000000000000000 ) ) ;
#7527=ORIENTED_EDGE ( 'NONE', *, *, #19028, .T. ) ;
#7529=DIRECTION ( 'NONE',  ( -1.000000000000000000, 0.000000000000000000, 0.000000000000000000 ) ) ;
#7538=DIRECTION ( 'NONE',  ( -1.000000000000000000, 0.000000000000000000, 0.000000000000000000 ) ) ;
#7543=CIRCLE ( 'NONE', #6407, 1.000000000000000888 ) ;
#7548=LINE ( 'NONE', #9498, #11894 ) ;
#7553=ORIENTED_EDGE ( 'NONE', *, *, #3348, .T. ) ;
#7557=ORIENTED_EDGE ( 'NONE', *, *, #17594, .T. ) ;
#7559=AXIS2_PLACEMENT_3D ( 'NONE', #12934, #18099, #3448 ) ;
#7560=CARTESIAN_POINT ( 'NONE',  ( -23.90000000000000213, 29.49999999999999645, 11.50000000000000000 ) ) ;
#7564=DIRECTION ( 'NONE',  ( 1.000000000000000000, 0.000000000000000000, 0.000000000000000000 ) ) ;
#7571=VECTOR ( 'NONE', #21149, 1000.000000000000000 ) ;
#7572=CARTESIAN_POINT ( 'NONE',  ( 29.00000000000000000, -29.50000000000000355, 11.00000000000000000 ) ) ;
#7580=LINE ( 'NONE', #15029, #11068 ) ;
#7581=EDGE_CURVE ( 'NONE', #1636, #3226, #1865, .T. ) ;
#7597=VERTEX_POINT ( 'NONE', #18461 ) ;
#7598=VERTEX_POINT ( 'NONE', #15129 ) ;
#7617=DIRECTION ( 'NONE',  ( 0.4828336235133042775, -0.8757121056631643752, 0.000000000000000000 ) ) ;
#7621=PRODUCT_DEFINITION_SHAPE ( 'NONE', 'NONE',  #8989 ) ;
#7622=EDGE_CURVE ( 'NONE', #5720, #11259, #493, .T. ) ;
#7634=CIRCLE ( 'NONE', #21303, 0.9999999999999994449 ) ;
#7639=ORIENTED_EDGE ( 'NONE', *, *, #16998, .F. ) ;
#7645=ADVANCED_FACE ( 'NONE', ( #13186 ), #11330, .F. ) ;
#7655=DIRECTION ( 'NONE',  ( 1.000000000000000000, 0.000000000000000000, 0.000000000000000000 ) ) ;
#7666=ORIENTED_EDGE ( 'NONE', *, *, #18003, .T. ) ;
#7670=FACE_OUTER_BOUND ( 'NONE', #15966, .T. ) ;
#7678=EDGE_LOOP ( 'NONE', ( #19815, #3567, #7482, #5002 ) ) ;
#7682=DIRECTION ( 'NONE',  ( 0.000000000000000000, 0.000000000000000000, -1.000000000000000000 ) ) ;
#7689=DIRECTION ( 'NONE',  ( -0.000000000000000000, 1.000000000000000000, -0.000000000000000000 ) ) ;
#7691=DIRECTION ( 'NONE',  ( -0.000000000000000000, 0.000000000000000000, 1.000000000000000000 ) ) ;
#7707=DIRECTION ( 'NONE',  ( -0.000000000000000000, -0.000000000000000000, -1.000000000000000000 ) ) ;
#7711=FACE_BOUND ( 'NONE', #11907, .T. ) ;
#7725=EDGE_CURVE ( 'NONE', #23989, #19319, #9066, .T. ) ;
#7729=VERTEX_POINT ( 'NONE', #4670 ) ;
#7738=DIRECTION ( 'NONE',  ( -0.000000000000000000, -0.000000000000000000, -1.000000000000000000 ) ) ;
#7751=ADVANCED_FACE ( 'NONE', ( #22222 ), #12185, .T. ) ;
#7754=ORIENTED_EDGE ( 'NONE', *, *, #14628, .T. ) ;
#7775=VECTOR ( 'NONE', #8653, 1000.000000000000000 ) ;
#7782=DIRECTION ( 'NONE',  ( -0.000000000000000000, 0.000000000000000000, 1.000000000000000000 ) ) ;
#7794=CYLINDRICAL_SURFACE ( 'NONE', #10510, 1.000000000000000888 ) ;
#7806=DIRECTION ( 'NONE',  ( 0.000000000000000000, 0.000000000000000000, -1.000000000000000000 ) ) ;
#7808=CIRCLE ( 'NONE', #21084, 1.000000000000000888 ) ;
#7816=ORIENTED_EDGE ( 'NONE', *, *, #19144, .F. ) ;
#7829=EDGE_CURVE ( 'NONE', #13833, #4922, #7203, .T. ) ;
#7830=DIRECTION ( 'NONE',  ( 1.000000000000000000, 0.000000000000000000, -0.000000000000000000 ) ) ;
#7832=EDGE_CURVE ( 'NONE', #666, #15840, #7885, .T. ) ;
#7837=FACE_OUTER_BOUND ( 'NONE', #7976, .T. ) ;
#7843=DIRECTION ( 'NONE',  ( 1.000000000000000000, 4.163336342344333082E-15, 0.000000000000000000 ) ) ;
#7846=DIRECTION ( 'NONE',  ( -0.000000000000000000, -0.000000000000000000, 1.000000000000000000 ) ) ;
#7856=AXIS2_PLACEMENT_3D ( 'NONE', #5344, #23537, #6816 ) ;
#7857=DIRECTION ( 'NONE',  ( 3.469446951953610639E-15, -1.000000000000000000, 0.000000000000000000 ) ) ;
#7862=CIRCLE ( 'NONE', #21541, 10.00000000000000888 ) ;
#7874=DIRECTION ( 'NONE',  ( 1.000000000000000000, 0.000000000000000000, 0.000000000000000000 ) ) ;
#7881=AXIS2_PLACEMENT_3D ( 'NONE', #22393, #7956, #9910 ) ;
#7882=ORIENTED_EDGE ( 'NONE', *, *, #3030, .T. ) ;
#7884=CARTESIAN_POINT ( 'NONE',  ( 23.90000000000000568, -29.50000000000000355, 11.50000000000000000 ) ) ;
#7885=CIRCLE ( 'NONE', #8279, 5.099999999999996980 ) ;
#7888=ORIENTED_EDGE ( 'NONE', *, *, #13051, .T. ) ;
#7893=ADVANCED_FACE ( 'NONE', ( #19040 ), #17066, .F. ) ;
#7898=AXIS2_PLACEMENT_3D ( 'NONE', #14093, #10054, #2642 ) ;
#7902=EDGE_LOOP ( 'NONE', ( #10845, #17501, #11988, #7639 ) ) ;
#7909=DIRECTION ( 'NONE',  ( 0.000000000000000000, 1.000000000000000000, -0.000000000000000000 ) ) ;
#7912=CARTESIAN_POINT ( 'NONE',  ( -30.00000000000000355, -3.851859888774471706E-31, 9.500000000000000000 ) ) ;
#7928=LINE ( 'NONE', #15377, #3640 ) ;
#7932=CARTESIAN_POINT ( 'NONE',  ( -29.00000000000000000, 29.49999999999999645, 12.00000000000000000 ) ) ;
#7934=FACE_OUTER_BOUND ( 'NONE', #16037, .T. ) ;
#7956=DIRECTION ( 'NONE',  ( 0.000000000000000000, 1.000000000000000000, 0.000000000000000000 ) ) ;
#7958=AXIS2_PLACEMENT_3D ( 'NONE', #19526, #176, #10232 ) ;
#7959=PRODUCT_DEFINITION_CONTEXT ( 'detailed design', #15693, 'design' ) ;
#7962=VERTEX_POINT ( 'NONE', #23634 ) ;
#7970=AXIS2_PLACEMENT_3D ( 'NONE', #19553, #9783, #4216 ) ;
#7971=ORIENTED_EDGE ( 'NONE', *, *, #21097, .F. ) ;
#7976=EDGE_LOOP ( 'NONE', ( #17831, #5180, #21034, #4217 ) ) ;
#7992=ORIENTED_EDGE ( 'NONE', *, *, #8444, .T. ) ;
#7996=AXIS2_PLACEMENT_3D ( 'NONE', #24040, #12803, #20152 ) ;
#8005=AXIS2_PLACEMENT_3D ( 'NONE', #5978, #22344, #13412 ) ;
#8012=LINE ( 'NONE', #9828, #9548 ) ;
#8013=EDGE_CURVE ( 'NONE', #15214, #7598, #22715, .T. ) ;
#8019=AXIS2_PLACEMENT_3D ( 'NONE', #5205, #16302, #10559 ) ;
#8044=PLANE ( 'NONE',  #21515 ) ;
#8048=DIRECTION ( 'NONE',  ( 0.000000000000000000, 1.000000000000000000, 0.000000000000000000 ) ) ;
#8055=DIRECTION ( 'NONE',  ( -0.000000000000000000, 0.000000000000000000, 1.000000000000000000 ) ) ;
#8058=EDGE_CURVE ( 'NONE', #4885, #19209, #2844, .T. ) ;
#8062=VERTEX_POINT ( 'NONE', #7560 ) ;
#8065=ORIENTED_EDGE ( 'NONE', *, *, #6436, .T. ) ;
#8094=CONICAL_SURFACE ( 'NONE', #11201, 2.024999999999999911, 0.7853981633974743692 ) ;
#8105=ORIENTED_EDGE ( 'NONE', *, *, #10676, .T. ) ;
#8118=EDGE_CURVE ( 'NONE', #21512, #14945, #12959, .T. ) ;
#8131=DIRECTION ( 'NONE',  ( 1.000000000000000000, -2.600433232233976523E-16, 0.000000000000000000 ) ) ;
#8132=CARTESIAN_POINT ( 'NONE',  ( -42.00000000000001421, -26.82133436441677432, 11.58578643762690596 ) ) ;
#8133=CARTESIAN_POINT ( 'NONE',  ( 20.99999999999999645, -29.50000000000000355, 11.50000000000000000 ) ) ;
#8135=FACE_OUTER_BOUND ( 'NONE', #3560, .T. ) ;
#8136=ADVANCED_FACE ( 'NONE', ( #17835 ), #6488, .F. ) ;
#8142=DIRECTION ( 'NONE',  ( 1.000000000000000000, 2.600433232233976523E-16, 0.000000000000000000 ) ) ;
#8162=CARTESIAN_POINT ( 'NONE',  ( 41.00000000000000000, 0.000000000000000000, 11.00000000000000000 ) ) ;
#8169=VERTEX_POINT ( 'NONE', #6355 ) ;
#8182=ORIENTED_EDGE ( 'NONE', *, *, #4791, .T. ) ;
#8184=FACE_BOUND ( 'NONE', #23595, .T. ) ;
#8188=ORIENTED_EDGE ( 'NONE', *, *, #10738, .T. ) ;
#8192=ADVANCED_FACE ( 'NONE', ( #15875 ), #3618, .T. ) ;
#8197=EDGE_CURVE ( 'NONE', #13932, #14909, #21556, .T. ) ;
#8200=ORIENTED_EDGE ( 'NONE', *, *, #7427, .F. ) ;
#8213=CARTESIAN_POINT ( 'NONE',  ( -34.00000000000000000, -3.851859888774471706E-31, 10.49999999999999822 ) ) ;
#8229=VERTEX_POINT ( 'NONE', #12679 ) ;
#8234=AXIS2_PLACEMENT_3D ( 'NONE', #2485, #9769, #5897 ) ;
#8237=ORIENTED_EDGE ( 'NONE', *, *, #21567, .F. ) ;
#8238=ORIENTED_EDGE ( 'NONE', *, *, #15769, .T. ) ;
#8242=EDGE_CURVE ( 'NONE', #15214, #3810, #1710, .T. ) ;
#8249=AXIS2_PLACEMENT_3D ( 'NONE', #14243, #24006, #16071 ) ;
#8251=EDGE_CURVE ( 'NONE', #17534, #22408, #1364, .T. ) ;
#8253=CARTESIAN_POINT ( 'NONE',  ( 33.99999999999998579, -1.387778780781445676E-14, 9.500000000000000000 ) ) ;
#8265=VERTEX_POINT ( 'NONE', #14388 ) ;
#8266=EDGE_LOOP ( 'NONE', ( #9906, #3155 ) ) ;
#8269=ORIENTED_EDGE ( 'NONE', *, *, #12322, .T. ) ;
#8279=AXIS2_PLACEMENT_3D ( 'NONE', #10846, #18316, #1597 ) ;
#8282=CIRCLE ( 'NONE', #4409, 5.999999999999998224 ) ;
#8313=LINE ( 'NONE', #13823, #6847 ) ;
#8314=AXIS2_PLACEMENT_3D ( 'NONE', #11616, #19083, #9772 ) ;
#8319=ORIENTED_EDGE ( 'NONE', *, *, #2738, .T. ) ;
#8338=VECTOR ( 'NONE', #15887, 1000.000000000000000 ) ;
#8341=ORIENTED_EDGE ( 'NONE', *, *, #5608, .F. ) ;
#8342=ADVANCED_FACE ( 'NONE', ( #13267 ), #16703, .T. ) ;
#8349=CARTESIAN_POINT ( 'NONE',  ( 0.000000000000000000, 0.000000000000000000, 12.00000000000000000 ) ) ;
#8350=DIRECTION ( 'NONE',  ( 0.000000000000000000, 0.000000000000000000, -1.000000000000000000 ) ) ;
#8362=AXIS2_PLACEMENT_3D ( 'NONE', #27, #19504, #9375 ) ;
#8364=AXIS2_PLACEMENT_3D ( 'NONE', #9717, #18901, #2052 ) ;
#8367=ORIENTED_EDGE ( 'NONE', *, *, #23289, .F. ) ;
#8386=ORIENTED_EDGE ( 'NONE', *, *, #15393, .F. ) ;
#8390=DIRECTION ( 'NONE',  ( -1.000000000000000000, -2.600433232233976523E-16, 0.000000000000000000 ) ) ;
#8395=CARTESIAN_POINT ( 'NONE',  ( 20.85000000000000497, -16.67999999999999616, 13.50000000000000178 ) ) ;
#8409=DIRECTION ( 'NONE',  ( 0.000000000000000000, -1.000000000000000000, 0.000000000000000000 ) ) ;
#8415=DIRECTION ( 'NONE',  ( 0.000000000000000000, 0.000000000000000000, 1.000000000000000000 ) ) ;
#8419=VECTOR ( 'NONE', #23906, 1000.000000000000000 ) ;
#8421=ORIENTED_EDGE ( 'NONE', *, *, #6346, .F. ) ;
#8422=CARTESIAN_POINT ( 'NONE',  ( 41.00000000000000000, 5.999999999999986677, 11.00000000000000000 ) ) ;
#8427=AXIS2_PLACEMENT_3D ( 'NONE', #8532, #19663, #2938 ) ;
#8430=DIRECTION ( 'NONE',  ( 0.000000000000000000, -0.000000000000000000, -1.000000000000000000 ) ) ;
#8431=ORIENTED_EDGE ( 'NONE', *, *, #14831, .F. ) ;
#8433=CARTESIAN_POINT ( 'NONE',  ( 42.00000000000000711, -26.82133436441677077, 11.58578643762690241 ) ) ;
#8434=VERTEX_POINT ( 'NONE', #2419 ) ;
#8441=CARTESIAN_POINT ( 'NONE',  ( -29.00000000000000000, -29.49999999999999645, 12.00000000000000000 ) ) ;
#8443=CARTESIAN_POINT ( 'NONE',  ( -1.999999999999994449, -45.00000000000000000, 0.02500000000000418554 ) ) ;
#8444=EDGE_CURVE ( 'NONE', #8229, #5720, #17429, .T. ) ;
#8445=VERTEX_POINT ( 'NONE', #8395 ) ;
#8456=TOROIDAL_SURFACE ( 'NONE', #20936, 3.999999999999999112, 1.000000000000000000 ) ;
#8459=CARTESIAN_POINT ( 'NONE',  ( 33.99999999999998579, -1.387778780781445676E-14, 11.00000000000000000 ) ) ;
#8465=EDGE_LOOP ( 'NONE', ( #9544, #12396 ) ) ;
#8466=DIRECTION ( 'NONE',  ( 1.000000000000000000, -2.600433232233976523E-16, 0.000000000000000000 ) ) ;
#8467=DIRECTION ( 'NONE',  ( -0.000000000000000000, -0.000000000000000000, -1.000000000000000000 ) ) ;
#8473=EDGE_CURVE ( 'NONE', #411, #22901, #23421, .T. ) ;
#8477=CARTESIAN_POINT ( 'NONE',  ( 29.00000000000000000, 29.50000000000000355, 11.00000000000000000 ) ) ;
#8479=CARTESIAN_POINT ( 'NONE',  ( 39.00000000000000000, 0.000000000000000000, 12.00000000000000000 ) ) ;
#8481=VERTEX_POINT ( 'NONE', #14017 ) ;
#8489=AXIS2_PLACEMENT_3D ( 'NONE', #1796, #14290, #16546 ) ;
#8496=ORIENTED_EDGE ( 'NONE', *, *, #21946, .F. ) ;
#8503=ORIENTED_EDGE ( 'NONE', *, *, #7354, .F. ) ;
#8532=CARTESIAN_POINT ( 'NONE',  ( -41.00000000000000000, -4.000000000000000888, 10.49999999999999822 ) ) ;
#8543=ADVANCED_FACE ( 'NONE', ( #8135 ), #21581, .T. ) ;
#8546=DIRECTION ( 'NONE',  ( 1.000000000000000000, 0.000000000000000000, 0.000000000000000000 ) ) ;
#8548=AXIS2_PLACEMENT_3D ( 'NONE', #4047, #505, #22846 ) ;
#8551=DIRECTION ( 'NONE',  ( -0.000000000000000000, -0.000000000000000000, -1.000000000000000000 ) ) ;
#8560=AXIS2_PLACEMENT_3D ( 'NONE', #1239, #12066, #16110 ) ;
#8561=ORIENTED_EDGE ( 'NONE', *, *, #5963, .F. ) ;
#8562=LINE ( 'NONE', #1033, #14737 ) ;
#8565=ORIENTED_EDGE ( 'NONE', *, *, #21568, .F. ) ;
#8567=ADVANCED_FACE ( 'NONE', ( #10570 ), #1638, .T. ) ;
#8570=CARTESIAN_POINT ( 'NONE',  ( -34.00000000000000000, -3.851859888774471706E-31, 9.500000000000000000 ) ) ;
#8573=ORIENTED_EDGE ( 'NONE', *, *, #9196, .T. ) ;
#8579=CARTESIAN_POINT ( 'NONE',  ( -34.00000000000000000, -4.999999999999999112, 11.00000000000000000 ) ) ;
#8580=CARTESIAN_POINT ( 'NONE',  ( -28.27483331787888332, -41.23752903419610050, 12.00000000000000000 ) ) ;
#8583=ORIENTED_EDGE ( 'NONE', *, *, #16821, .T. ) ;
#8585=DIRECTION ( 'NONE',  ( 0.000000000000000000, -1.000000000000000000, 0.000000000000000000 ) ) ;
#8588=CYLINDRICAL_SURFACE ( 'NONE', #10354, 8.000000000000003553 ) ;
#8609=EDGE_LOOP ( 'NONE', ( #15670, #17063, #24069, #11580 ) ) ;
#8610=DIRECTION ( 'NONE',  ( -1.000000000000000000, 0.000000000000000000, 0.000000000000000000 ) ) ;
#8620=DIRECTION ( 'NONE',  ( 1.000000000000000000, 0.000000000000000000, -0.000000000000000000 ) ) ;
#8642=AXIS2_PLACEMENT_3D ( 'NONE', #23443, #15871, #6601 ) ;
#8644=CIRCLE ( 'NONE', #18015, 1.000000000000000888 ) ;
#8653=DIRECTION ( 'NONE',  ( -0.000000000000000000, -0.000000000000000000, 1.000000000000000000 ) ) ;
#8666=CIRCLE ( 'NONE', #16840, 4.999999999999997335 ) ;
#8670=DIRECTION ( 'NONE',  ( -1.000000000000000000, 0.000000000000000000, 0.000000000000000000 ) ) ;
#8673=DIRECTION ( 'NONE',  ( 0.000000000000000000, 0.000000000000000000, -1.000000000000000000 ) ) ;
#8684=AXIS2_PLACEMENT_3D ( 'NONE', #19957, #19739, #21796 ) ;
#8699=AXIS2_PLACEMENT_3D ( 'NONE', #4943, #21148, #14072 ) ;
#8706=EDGE_CURVE ( 'NONE', #19009, #2972, #16102, .T. ) ;
#8708=DIRECTION ( 'NONE',  ( 0.000000000000000000, -1.000000000000000000, 0.000000000000000000 ) ) ;
#8711=CARTESIAN_POINT ( 'NONE',  ( 33.99999999999998579, 5.999999999999985789, 11.00000000000000000 ) ) ;
#8712=DIRECTION ( 'NONE',  ( -1.000000000000000000, 0.000000000000000000, 0.000000000000000000 ) ) ;
#8713=VERTEX_POINT ( 'NONE', #14829 ) ;
#8717=CARTESIAN_POINT ( 'NONE',  ( -0.9830802669677229932, 45.00000000000000000, 0.02500000000000418554 ) ) ;
#8725=LINE ( 'NONE', #6913, #18851 ) ;
#8727=LINE ( 'NONE', #7261, #23908 ) ;
#8728=CIRCLE ( 'NONE', #22383, 1.500000000000001332 ) ;
#8747=DIRECTION ( 'NONE',  ( 0.000000000000000000, 1.000000000000000000, -0.000000000000000000 ) ) ;
#8753=CONICAL_SURFACE ( 'NONE', #6018, 1.999999999999994449, 1.029744258676653201 ) ;
#8755=ORIENTED_EDGE ( 'NONE', *, *, #1629, .T. ) ;
#8758=CIRCLE ( 'NONE', #12269, 5.999999999999998224 ) ;
#8760=VERTEX_POINT ( 'NONE', #13009 ) ;
#8761=CARTESIAN_POINT ( 'NONE',  ( 1.016919733032271456, 45.00000000000000000, 3.000000000000002665 ) ) ;
#8767=ORIENTED_EDGE ( 'NONE', *, *, #1998, .T. ) ;
#8780=DIRECTION ( 'NONE',  ( 0.4828336235133043330, -0.8757121056631641531, 0.000000000000000000 ) ) ;
#8791=CIRCLE ( 'NONE', #4135, 2.000000000000000000 ) ;
#8794=ORIENTED_EDGE ( 'NONE', *, *, #12758, .F. ) ;
#8797=ORIENTED_EDGE ( 'NONE', *, *, #6470, .F. ) ;
#8804=CARTESIAN_POINT ( 'NONE',  ( 41.00000000000000000, -26.23076770084981391, 12.00000000000000000 ) ) ;
#8806=AXIS2_PLACEMENT_3D ( 'NONE', #16389, #1767, #9193 ) ;
#8811=DIRECTION ( 'NONE',  ( -0.000000000000000000, -0.000000000000000000, 1.000000000000000000 ) ) ;
#8822=EDGE_CURVE ( 'NONE', #12778, #17472, #21318, .T. ) ;
#8829=EDGE_LOOP ( 'NONE', ( #11520, #1999, #22604, #21133 ) ) ;
#8849=EDGE_CURVE ( 'NONE', #12921, #3740, #9788, .T. ) ;
#8864=CARTESIAN_POINT ( 'NONE',  ( -29.00000000000000000, 29.49999999999999645, 11.00000000000000000 ) ) ;
#8866=EDGE_CURVE ( 'NONE', #23300, #19009, #7130, .T. ) ;
#8869=ORIENTED_EDGE ( 'NONE', *, *, #17076, .T. ) ;
#8870=DIRECTION ( 'NONE',  ( -6.938893903907221278E-15, 1.000000000000000000, 6.938893903907221278E-15 ) ) ;
#8874=CARTESIAN_POINT ( 'NONE',  ( -30.00000000000000355, -3.851859888774471706E-31, 10.49999999999999822 ) ) ;
#8881=CYLINDRICAL_SURFACE ( 'NONE', #23797, 1.500000000000001332 ) ;
#8908=CLOSED_SHELL ( 'NONE', ( #12140, #6015, #18998, #4175, #11538, #1127, #11921, #24028, #23383, #21479, #10214, #1552, #1511, #6212, #11714, #21229, #2555, #13446, #6347, #18062, #13467, #740, #4258, #6997, #4424, #21339, #15494, #1585, #16474, #4887, #2714, #13057, #12132, #20978, #1382, #13160, #21166, #18441, #23139, #17759, #10249, #2879, #10498, #23972, #18253, #1187, #11103, #6131, #10887, #1258, #8342, #9002, #22290, #7893, #23812, #21553, #5045, #5108, #9275, #9166, #7645, #18819, #8136, #14971, #3268, #19636, #11213, #19704, #14631, #16941, #8567, #15954, #18589, #508, #19877, #22517, #16408, #12648, #7506, #7751, #1435, #15633, #8543, #8192, #20926, #16943, #12104, #3537, #18280, #12138, #16914, #2009, #19860, #14765, #1071, #12235, #2556, #6707, #5339, #18115, #22935, #12032, #17025, #656, #21776, #20954, #23714, #5775, #19125, #571, #19787, #2187, #23032, #10065, #17493, #2316, #6738, #19243, #12351, #18709, #2240, #12052, #19754, #23787, #23435, #11029, #17046, #18684, #6415, #20900, #15064, #4096, #6960, #10888, #14786 ) ) ;
#8910=CARTESIAN_POINT ( 'NONE',  ( 40.77574956473004164, -27.49633847812775755, 0.000000000000000000 ) ) ;
#8922=CARTESIAN_POINT ( 'NONE',  ( -41.50000000000000000, 28.80990663662250739, 11.00000000000000000 ) ) ;
#8928=CARTESIAN_POINT ( 'NONE',  ( -34.00000000000000000, -5.999999999999999112, 11.00000000000000000 ) ) ;
#8933=ORIENTED_EDGE ( 'NONE', *, *, #10122, .T. ) ;
#8937=CARTESIAN_POINT ( 'NONE',  ( -41.00000000000000000, -5.000000000000000888, 9.500000000000000000 ) ) ;
#8940=ORIENTED_EDGE ( 'NONE', *, *, #1914, .T. ) ;
#8941=ORIENTED_EDGE ( 'NONE', *, *, #16550, .T. ) ;
#8946=CYLINDRICAL_SURFACE ( 'NONE', #8806, 1.000000000000002442 ) ;
#8966=DIRECTION ( 'NONE',  ( -0.000000000000000000, 0.000000000000000000, 1.000000000000000000 ) ) ;
#8975=LINE ( 'NONE', #5712, #19935 ) ;
#8979=DIRECTION ( 'NONE',  ( 1.000000000000000000, 0.000000000000000000, 0.000000000000000000 ) ) ;
#8989=PRODUCT_DEFINITION ( 'UNKNOWN', '', #13904, #7959 ) ;
#8994=PLANE ( 'NONE',  #10228 ) ;
#8996=CARTESIAN_POINT ( 'NONE',  ( -40.00000000000000000, 0.000000000000000000, 0.000000000000000000 ) ) ;
#8999=CARTESIAN_POINT ( 'NONE',  ( 41.00000000000000000, 0.000000000000000000, 11.00000000000000000 ) ) ;
#9000=FACE_OUTER_BOUND ( 'NONE', #413, .T. ) ;
#9001=CARTESIAN_POINT ( 'NONE',  ( 40.29291594121673370, 26.62062637246459218, 12.00000000000000000 ) ) ;
#9002=ADVANCED_FACE ( 'NONE', ( #23329 ), #21730, .F. ) ;
#9023=VECTOR ( 'NONE', #2552, 1000.000000000000000 ) ;
#9024=AXIS2_PLACEMENT_3D ( 'NONE', #1335, #3043, #12771 ) ;
#9029=CYLINDRICAL_SURFACE ( 'NONE', #12188, 11.00000000000000711 ) ;
#9030=EDGE_CURVE ( 'NONE', #20616, #12416, #10970, .T. ) ;
#9035=ORIENTED_EDGE ( 'NONE', *, *, #7159, .F. ) ;
#9039=CIRCLE ( 'NONE', #22688, 2.024999999999999911 ) ;
#9042=AXIS2_PLACEMENT_3D ( 'NONE', #17304, #2417, #15710 ) ;
#9043=CARTESIAN_POINT ( 'NONE',  ( 29.00000000000000000, 29.50000000000000355, 12.00000000000000000 ) ) ;
#9050=DIRECTION ( 'NONE',  ( -1.000000000000000000, 0.000000000000000000, 0.000000000000000000 ) ) ;
#9054=EDGE_LOOP ( 'NONE', ( #13822, #20218, #18917, #6253 ) ) ;
#9058=CIRCLE ( 'NONE', #4001, 1.000000000000000888 ) ;
#9064=FACE_OUTER_BOUND ( 'NONE', #16367, .T. ) ;
#9066=CIRCLE ( 'NONE', #11789, 2.024999999999999911 ) ;
#9071=CARTESIAN_POINT ( 'NONE',  ( -20.84999999999999787, -16.67999999999985050, 14.50000000000000000 ) ) ;
#9072=DIRECTION ( 'NONE',  ( -0.000000000000000000, -0.000000000000000000, -1.000000000000000000 ) ) ;
#9074=DIRECTION ( 'NONE',  ( -1.000000000000000000, 0.000000000000000000, 0.000000000000000000 ) ) ;
#9092=EDGE_CURVE ( 'NONE', #24045, #1813, #16798, .T. ) ;
#9095=CARTESIAN_POINT ( 'NONE',  ( -20.84999999999999787, 16.67999999999985405, 13.50000000000000178 ) ) ;
#9102=AXIS2_PLACEMENT_3D ( 'NONE', #9204, #12386, #9074 ) ;
#9106=VECTOR ( 'NONE', #22177, 1000.000000000000000 ) ;
#9113=ORIENTED_EDGE ( 'NONE', *, *, #6933, .T. ) ;
#9117=ORIENTED_EDGE ( 'NONE', *, *, #6248, .F. ) ;
#9126=VECTOR ( 'NONE', #6655, 1000.000000000000000 ) ;
#9127=TOROIDAL_SURFACE ( 'NONE', #22782, 5.999999999999999112, 1.000000000000000000 ) ;
#9134=CYLINDRICAL_SURFACE ( 'NONE', #935, 8.000000000000003553 ) ;
#9135=DIRECTION ( 'NONE',  ( 1.000000000000000000, 0.000000000000000000, 0.000000000000000000 ) ) ;
#9136=CYLINDRICAL_SURFACE ( 'NONE', #18887, 1.000000000000000888 ) ;
#9138=EDGE_CURVE ( 'NONE', #7050, #14193, #6086, .T. ) ;
#9143=ORIENTED_EDGE ( 'NONE', *, *, #10101, .T. ) ;
#9155=CARTESIAN_POINT ( 'NONE',  ( 40.00000000000000000, 29.49999999999999645, 0.000000000000000000 ) ) ;
#9156=DIRECTION ( 'NONE',  ( 1.000000000000000000, 3.469446951953611822E-15, 0.000000000000000000 ) ) ;
#9166=ADVANCED_FACE ( 'NONE', ( #723 ), #5960, .F. ) ;
#9175=CARTESIAN_POINT ( 'NONE',  ( 1.999999999999994449, -45.00000000000000000, 0.02500000000000418554 ) ) ;
#9178=( GEOMETRIC_REPRESENTATION_CONTEXT ( 3 ) GLOBAL_UNCERTAINTY_ASSIGNED_CONTEXT ( ( #9598 ) ) GLOBAL_UNIT_ASSIGNED_CONTEXT ( ( #20708, #18649, #11281 ) ) REPRESENTATION_CONTEXT ( 'NONE', 'WORKASPACE' ) );
#9180=ORIENTED_EDGE ( 'NONE', *, *, #4799, .T. ) ;
#9181=VERTEX_POINT ( 'NONE', #7884 ) ;
#9185=ORIENTED_EDGE ( 'NONE', *, *, #5504, .F. ) ;
#9193=DIRECTION ( 'NONE',  ( -0.4828336235133042775, 0.8757121056631643752, 0.000000000000000000 ) ) ;
#9196=EDGE_CURVE ( 'NONE', #20146, #16881, #20860, .T. ) ;
#9204=CARTESIAN_POINT ( 'NONE',  ( -41.00000000000000000, 6.000000000000000888, 10.49999999999999822 ) ) ;
#9207=VERTEX_POINT ( 'NONE', #466 ) ;
#9210=EDGE_LOOP ( 'NONE', ( #14314, #19219, #22224, #14913 ) ) ;
#9233=CARTESIAN_POINT ( 'NONE',  ( -34.00000000000000000, 3.999999999999999112, 9.500000000000000000 ) ) ;
#9236=DIRECTION ( 'NONE',  ( 1.000000000000000000, 0.000000000000000000, 0.000000000000000000 ) ) ;
#9241=ORIENTED_EDGE ( 'NONE', *, *, #17445, .F. ) ;
#9242=SHAPE_REPRESENTATION_RELATIONSHIP ( 'NONE' , 'NONE' ,  #19247, #9857 ) ;
#9252=CARTESIAN_POINT ( 'NONE',  ( -34.00000000000000000, -3.851859888774471706E-31, 9.500000000000000000 ) ) ;
#9257=VECTOR ( 'NONE', #3088, 1000.000000000000227 ) ;
#9265=FACE_OUTER_BOUND ( 'NONE', #19351, .T. ) ;
#9275=ADVANCED_FACE ( 'NONE', ( #6932 ), #14120, .F. ) ;
#9277=CARTESIAN_POINT ( 'NONE',  ( 42.00000000000000000, -6.000000000000015099, 10.49999999999999822 ) ) ;
#9280=SPHERICAL_SURFACE ( 'NONE', #17639, 1.000000000000000000 ) ;
#9287=PLANE ( 'NONE',  #19375 ) ;
#9303=CARTESIAN_POINT ( 'NONE',  ( -29.00000000000000000, -29.49999999999999645, 12.00000000000000000 ) ) ;
#9305=LINE ( 'NONE', #10666, #6079 ) ;
#9309=DIRECTION ( 'NONE',  ( -0.000000000000000000, 1.000000000000000000, -0.000000000000000000 ) ) ;
#9312=ORIENTED_EDGE ( 'NONE', *, *, #21074, .F. ) ;
#9313=AXIS2_PLACEMENT_3D ( 'NONE', #17772, #4487, #2644 ) ;
#9315=EDGE_CURVE ( 'NONE', #12921, #21260, #6577, .T. ) ;
#9317=ORIENTED_EDGE ( 'NONE', *, *, #8013, .F. ) ;
#9324=CARTESIAN_POINT ( 'NONE',  ( 29.00000000000000000, -29.50000000000000355, 11.50000000000000000 ) ) ;
#9332=DIRECTION ( 'NONE',  ( 0.000000000000000000, 0.000000000000000000, -1.000000000000000000 ) ) ;
#9339=ORIENTED_EDGE ( 'NONE', *, *, #17974, .F. ) ;
#9344=ORIENTED_EDGE ( 'NONE', *, *, #8473, .T. ) ;
#9346=DIRECTION ( 'NONE',  ( 0.000000000000000000, -1.000000000000000000, 0.000000000000000000 ) ) ;
#9350=ORIENTED_EDGE ( 'NONE', *, *, #22737, .F. ) ;
#9356=VERTEX_POINT ( 'NONE', #12509 ) ;
#9361=DIRECTION ( 'NONE',  ( -0.000000000000000000, 0.000000000000000000, 1.000000000000000000 ) ) ;
#9362=CARTESIAN_POINT ( 'NONE',  ( -19.84999999999999787, -16.67999999999985761, 14.50000000000000000 ) ) ;
#9364=EDGE_LOOP ( 'NONE', ( #23364, #2063, #16919, #11256 ) ) ;
#9366=CARTESIAN_POINT ( 'NONE',  ( 30.44534269664590553, 40.40463133211080304, 11.00000000000000000 ) ) ;
#9375=DIRECTION ( 'NONE',  ( 1.000000000000000000, 0.000000000000000000, 0.000000000000000000 ) ) ;
#9382=CARTESIAN_POINT ( 'NONE',  ( 40.77574956473004164, 27.49633847812775755, 0.000000000000000000 ) ) ;
#9387=CIRCLE ( 'NONE', #8642, 1.000000000000000000 ) ;
#9389=DIRECTION ( 'NONE',  ( 0.000000000000000000, 0.000000000000000000, 1.000000000000000000 ) ) ;
#9393=ORIENTED_EDGE ( 'NONE', *, *, #8118, .F. ) ;
#9402=VECTOR ( 'NONE', #8131, 1000.000000000000000 ) ;
#9403=CIRCLE ( 'NONE', #14491, 50.00000000000000000 ) ;
#9417=DIRECTION ( 'NONE',  ( -1.000000000000000000, 0.000000000000000000, 0.000000000000000000 ) ) ;
#9430=ORIENTED_EDGE ( 'NONE', *, *, #10628, .F. ) ;
#9431=EDGE_LOOP ( 'NONE', ( #18234, #9117, #341, #21988 ) ) ;
#9446=DIRECTION ( 'NONE',  ( -0.000000000000000000, 0.000000000000000000, 1.000000000000000000 ) ) ;
#9449=DIRECTION ( 'NONE',  ( 0.000000000000000000, 0.000000000000000000, 1.000000000000000000 ) ) ;
#9450=AXIS2_PLACEMENT_3D ( 'NONE', #14921, #66, #24091 ) ;
#9457=ORIENTED_EDGE ( 'NONE', *, *, #2880, .F. ) ;
#9462=EDGE_CURVE ( 'NONE', #16379, #23250, #2434, .T. ) ;
#9472=DIRECTION ( 'NONE',  ( 0.000000000000000000, -1.000000000000000000, 0.000000000000000000 ) ) ;
#9473=AXIS2_PLACEMENT_3D ( 'NONE', #672, #8466, #19343 ) ;
#9485=VERTEX_POINT ( 'NONE', #14824 ) ;
#9490=DIRECTION ( 'NONE',  ( 1.000000000000000000, 9.527085451588871562E-16, 0.000000000000000000 ) ) ;
#9498=CARTESIAN_POINT ( 'NONE',  ( 37.00000000000000711, -29.50000000000000355, 11.50000000000000000 ) ) ;
#9504=ORIENTED_EDGE ( 'NONE', *, *, #17306, .T. ) ;
#9508=ORIENTED_EDGE ( 'NONE', *, *, #6578, .T. ) ;
#9512=CARTESIAN_POINT ( 'NONE',  ( -41.00000000000000000, -6.000000000000000888, 12.00000000000000000 ) ) ;
#9514=CARTESIAN_POINT ( 'NONE',  ( 33.99999999999998579, -1.387778780781445676E-14, 10.49999999999999822 ) ) ;
#9517=DIRECTION ( 'NONE',  ( 0.000000000000000000, 1.000000000000000000, 0.000000000000000000 ) ) ;
#9528=DIRECTION ( 'NONE',  ( 1.000000000000000000, 0.000000000000000000, 0.000000000000000000 ) ) ;
#9530=VERTEX_POINT ( 'NONE', #22775 ) ;
#9532=VECTOR ( 'NONE', #11560, 1000.000000000000000 ) ;
#9533=ORIENTED_EDGE ( 'NONE', *, *, #18146, .F. ) ;
#9535=DIRECTION ( 'NONE',  ( 1.000000000000000000, 0.000000000000000000, 0.000000000000000000 ) ) ;
#9537=AXIS2_PLACEMENT_3D ( 'NONE', #18555, #3785, #1939 ) ;
#9539=CARTESIAN_POINT ( 'NONE',  ( -39.00000000000000000, 28.80990663662251805, 12.00000000000000000 ) ) ;
#9544=ORIENTED_EDGE ( 'NONE', *, *, #2605, .F. ) ;
#9548=VECTOR ( 'NONE', #23166, 1000.000000000000000 ) ;
#9553=DIRECTION ( 'NONE',  ( 0.1313947906041688374, -0.9913301211009815095, 0.000000000000000000 ) ) ;
#9554=ORIENTED_EDGE ( 'NONE', *, *, #5840, .T. ) ;
#9557=AXIS2_PLACEMENT_3D ( 'NONE', #14324, #14092, #2875 ) ;
#9560=ORIENTED_EDGE ( 'NONE', *, *, #23289, .T. ) ;
#9572=CYLINDRICAL_SURFACE ( 'NONE', #21557, 11.00000000000000711 ) ;
#9576=ORIENTED_EDGE ( 'NONE', *, *, #17301, .T. ) ;
#9585=CARTESIAN_POINT ( 'NONE',  ( -42.00000000000000711, 26.82133436441677077, 11.58578643762690241 ) ) ;
#9595=ORIENTED_EDGE ( 'NONE', *, *, #3511, .T. ) ;
#9598=UNCERTAINTY_MEASURE_WITH_UNIT (LENGTH_MEASURE( 1.000000000000000082E-05 ), #20708, 'distance_accuracy_value', 'NONE');
#9602=DIRECTION ( 'NONE',  ( -0.000000000000000000, 0.000000000000000000, 1.000000000000000000 ) ) ;
#9621=DIRECTION ( 'NONE',  ( -0.000000000000000000, 0.000000000000000000, 1.000000000000000000 ) ) ;
#9623=DIRECTION ( 'NONE',  ( -0.000000000000000000, -1.000000000000000000, -0.000000000000000000 ) ) ;
#9635=CIRCLE ( 'NONE', #10803, 1.000000000000000888 ) ;
#9638=CYLINDRICAL_SURFACE ( 'NONE', #19075, 1.000000000000000000 ) ;
#9640=DIRECTION ( 'NONE',  ( -0.000000000000000000, 1.000000000000000000, -0.000000000000000000 ) ) ;
#9641=DIRECTION ( 'NONE',  ( 0.000000000000000000, -1.000000000000000000, 0.000000000000000000 ) ) ;
#9656=AXIS2_PLACEMENT_3D ( 'NONE', #18697, #3927, #11596 ) ;
#9660=ORIENTED_EDGE ( 'NONE', *, *, #12749, .F. ) ;
#9673=ORIENTED_EDGE ( 'NONE', *, *, #8197, .T. ) ;
#9677=CARTESIAN_POINT ( 'NONE',  ( 29.00000000000000000, -29.50000000000000355, 12.00000000000000000 ) ) ;
#9682=DIRECTION ( 'NONE',  ( 0.000000000000000000, -0.000000000000000000, -1.000000000000000000 ) ) ;
#9703=ORIENTED_EDGE ( 'NONE', *, *, #2089, .F. ) ;
#9704=CARTESIAN_POINT ( 'NONE',  ( 40.00000000000000000, 28.80990663662251450, 11.00000000000000000 ) ) ;
#9713=LINE ( 'NONE', #4710, #11372 ) ;
#9717=CARTESIAN_POINT ( 'NONE',  ( 0.000000000000000000, 0.000000000000000000, 12.00000000000000000 ) ) ;
#9721=ORIENTED_EDGE ( 'NONE', *, *, #7213, .F. ) ;
#9725=DIRECTION ( 'NONE',  ( 2.600433232233976523E-16, -1.000000000000000000, 0.000000000000000000 ) ) ;
#9731=CARTESIAN_POINT ( 'NONE',  ( 33.99999999999998579, 4.999999999999985789, 9.500000000000000000 ) ) ;
#9738=DIRECTION ( 'NONE',  ( 1.000000000000000000, 0.000000000000000000, -0.000000000000000000 ) ) ;
#9746=CARTESIAN_POINT ( 'NONE',  ( 42.00000000000000000, -6.000000000000015099, 11.00000000000000000 ) ) ;
#9747=EDGE_CURVE ( 'NONE', #3762, #21057, #18448, .T. ) ;
#9758=EDGE_CURVE ( 'NONE', #6894, #12373, #6780, .T. ) ;
#9759=CIRCLE ( 'NONE', #4743, 1.000000000000000888 ) ;
#9763=VERTEX_POINT ( 'NONE', #10429 ) ;
#9764=CARTESIAN_POINT ( 'NONE',  ( -37.00000000000000711, -29.49999999999999645, 12.00000000000000000 ) ) ;
#9765=ORIENTED_EDGE ( 'NONE', *, *, #622, .T. ) ;
#9769=DIRECTION ( 'NONE',  ( 0.000000000000000000, 0.000000000000000000, 1.000000000000000000 ) ) ;
#9770=DIRECTION ( 'NONE',  ( -0.000000000000000000, 0.000000000000000000, 1.000000000000000000 ) ) ;
#9772=DIRECTION ( 'NONE',  ( 1.000000000000000000, 0.000000000000000000, 0.000000000000000000 ) ) ;
#9774=ORIENTED_EDGE ( 'NONE', *, *, #7832, .T. ) ;
#9777=EDGE_LOOP ( 'NONE', ( #1621, #14430, #18857, #21412 ) ) ;
#9780=ORIENTED_EDGE ( 'NONE', *, *, #17214, .T. ) ;
#9781=ORIENTED_EDGE ( 'NONE', *, *, #21946, .T. ) ;
#9783=DIRECTION ( 'NONE',  ( -0.000000000000000000, -0.000000000000000000, -1.000000000000000000 ) ) ;
#9786=EDGE_LOOP ( 'NONE', ( #2694, #19894, #16434, #3897 ) ) ;
#9787=EDGE_LOOP ( 'NONE', ( #8869, #23549, #16562, #21326 ) ) ;
#9788=CIRCLE ( 'NONE', #16050, 1.999999999999994449 ) ;
#9789=AXIS2_PLACEMENT_3D ( 'NONE', #9991, #14150, #15979 ) ;
#9805=CARTESIAN_POINT ( 'NONE',  ( -20.64923905428956630, -37.45138642374539728, 11.00000000000000000 ) ) ;
#9808=EDGE_CURVE ( 'NONE', #12373, #2607, #5973, .T. ) ;
#9825=CARTESIAN_POINT ( 'NONE',  ( -20.99999999999999645, 29.49999999999999645, 12.00000000000000000 ) ) ;
#9828=CARTESIAN_POINT ( 'NONE',  ( -42.00000000000000000, 5.000000000000000888, 11.00000000000000000 ) ) ;
#9846=EDGE_CURVE ( 'NONE', #3762, #9763, #22339, .T. ) ;
#9853=AXIS2_PLACEMENT_3D ( 'NONE', #19871, #16205, #18036 ) ;
#9856=CIRCLE ( 'NONE', #16113, 2.500000000000002220 ) ;
#9857=ADVANCED_BREP_SHAPE_REPRESENTATION ( '', ( #2277, #8005 ), #9178 ) ;
#9864=VECTOR ( 'NONE', #18541, 1000.000000000000000 ) ;
#9874=CIRCLE ( 'NONE', #13004, 8.000000000000003553 ) ;
#9877=CIRCLE ( 'NONE', #14178, 4.999999999999997335 ) ;
#9885=CIRCLE ( 'NONE', #2895, 1.000000000000000888 ) ;
#9894=ORIENTED_EDGE ( 'NONE', *, *, #16439, .T. ) ;
#9900=CIRCLE ( 'NONE', #15755, 20.85000000000000142 ) ;
#9906=ORIENTED_EDGE ( 'NONE', *, *, #11291, .T. ) ;
#9909=DIRECTION ( 'NONE',  ( -0.5654966663575777819, -0.8247505806839220410, 0.000000000000000000 ) ) ;
#9910=DIRECTION ( 'NONE',  ( 1.000000000000000000, 0.000000000000000000, 0.000000000000000000 ) ) ;
#9917=DIRECTION ( 'NONE',  ( 0.000000000000000000, 0.000000000000000000, -1.000000000000000000 ) ) ;
#9920=ORIENTED_EDGE ( 'NONE', *, *, #8118, .T. ) ;
#9925=VERTEX_POINT ( 'NONE', #2080 ) ;
#9926=VERTEX_POINT ( 'NONE', #23742 ) ;
#9935=LINE ( 'NONE', #931, #16333 ) ;
#9939=VECTOR ( 'NONE', #5982, 1000.000000000000000 ) ;
#9953=ORIENTED_EDGE ( 'NONE', *, *, #20484, .T. ) ;
#9954=DIRECTION ( 'NONE',  ( 0.000000000000000000, 0.000000000000000000, 1.000000000000000000 ) ) ;
#9969=CARTESIAN_POINT ( 'NONE',  ( 37.00000000000000711, -29.50000000000000355, 12.00000000000000000 ) ) ;
#9977=ORIENTED_EDGE ( 'NONE', *, *, #20017, .F. ) ;
#9982=TOROIDAL_SURFACE ( 'NONE', #1458, 19.84999999999999787, 1.000000000000000000 ) ;
#9991=CARTESIAN_POINT ( 'NONE',  ( 0.000000000000000000, -45.00000000000000000, 0.02500000000000418554 ) ) ;
#9993=VERTEX_POINT ( 'NONE', #4546 ) ;
#9996=CARTESIAN_POINT ( 'NONE',  ( -29.00000000000000000, -29.49999999999999645, 11.50000000000000000 ) ) ;
#9998=CARTESIAN_POINT ( 'NONE',  ( -21.13207267780287069, -38.32709852940855910, 11.00000000000000000 ) ) ;
#10005=DIRECTION ( 'NONE',  ( -0.000000000000000000, -0.000000000000000000, -1.000000000000000000 ) ) ;
#10017=EDGE_LOOP ( 'NONE', ( #20237, #13082, #21053, #17586 ) ) ;
#10021=ORIENTED_EDGE ( 'NONE', *, *, #1836, .F. ) ;
#10023=DIRECTION ( 'NONE',  ( 1.000000000000000000, 0.000000000000000000, 0.000000000000000000 ) ) ;
#10027=DIRECTION ( 'NONE',  ( 1.000000000000000000, 0.000000000000000000, 0.000000000000000000 ) ) ;
#10032=AXIS2_PLACEMENT_3D ( 'NONE', #14461, #22287, #18025 ) ;
#10054=DIRECTION ( 'NONE',  ( 0.000000000000000000, -1.000000000000000000, 0.000000000000000000 ) ) ;
#10055=ORIENTED_EDGE ( 'NONE', *, *, #17628, .T. ) ;
#10063=CARTESIAN_POINT ( 'NONE',  ( 39.00000000000000000, -29.49999999999999645, 12.00000000000000000 ) ) ;
#10065=ADVANCED_FACE ( 'NONE', ( #11694 ), #14919, .T. ) ;
#10069=AXIS2_PLACEMENT_3D ( 'NONE', #17836, #6489, #10111 ) ;
#10071=EDGE_LOOP ( 'NONE', ( #2650, #3877, #8182, #8583 ) ) ;
#10088=DIRECTION ( 'NONE',  ( 1.000000000000000000, -0.000000000000000000, 0.000000000000000000 ) ) ;
#10090=EDGE_LOOP ( 'NONE', ( #4784, #11819, #22824, #21038 ) ) ;
#10092=ORIENTED_EDGE ( 'NONE', *, *, #817, .F. ) ;
#10093=EDGE_LOOP ( 'NONE', ( #11716, #8797, #16270, #22681 ) ) ;
#10097=AXIS2_PLACEMENT_3D ( 'NONE', #3601, #23988, #1784 ) ;
#10100=DIRECTION ( 'NONE',  ( -0.000000000000000000, -0.000000000000000000, -1.000000000000000000 ) ) ;
#10101=EDGE_CURVE ( 'NONE', #9181, #21814, #7064, .T. ) ;
#10111=DIRECTION ( 'NONE',  ( 0.000000000000000000, 1.000000000000000000, 0.000000000000000000 ) ) ;
#10122=EDGE_CURVE ( 'NONE', #4241, #555, #17677, .T. ) ;
#10127=ORIENTED_EDGE ( 'NONE', *, *, #20075, .F. ) ;
#10157=ORIENTED_EDGE ( 'NONE', *, *, #15449, .F. ) ;
#10166=CYLINDRICAL_SURFACE ( 'NONE', #10992, 1.000000000000000888 ) ;
#10168=CIRCLE ( 'NONE', #11710, 0.9999999999999994449 ) ;
#10187=AXIS2_PLACEMENT_3D ( 'NONE', #2119, #4203, #15267 ) ;
#10196=ORIENTED_EDGE ( 'NONE', *, *, #13323, .F. ) ;
#10197=DIRECTION ( 'NONE',  ( -0.000000000000000000, -0.000000000000000000, -1.000000000000000000 ) ) ;
#10203=LINE ( 'NONE', #17665, #15354 ) ;
#10208=AXIS2_PLACEMENT_3D ( 'NONE', #2486, #15520, #9909 ) ;
#10209=TOROIDAL_SURFACE ( 'NONE', #12543, 2.500000000000001776, 1.000000000000000000 ) ;
#10211=EDGE_CURVE ( 'NONE', #8434, #977, #250, .T. ) ;
#10214=ADVANCED_FACE ( 'NONE', ( #1832 ), #9134, .F. ) ;
#10216=VERTEX_POINT ( 'NONE', #20493 ) ;
#10221=DIRECTION ( 'NONE',  ( -0.8247505806839219300, -0.5654966663575777819, 2.861428388275804004E-15 ) ) ;
#10224=AXIS2_PLACEMENT_3D ( 'NONE', #20624, #18780, #5855 ) ;
#10226=CARTESIAN_POINT ( 'NONE',  ( -0.9830802669677229932, 45.00000000000000000, 0.000000000000000000 ) ) ;
#10228=AXIS2_PLACEMENT_3D ( 'NONE', #22088, #5360, #16567 ) ;
#10230=VECTOR ( 'NONE', #5102, 1000.000000000000000 ) ;
#10232=DIRECTION ( 'NONE',  ( -0.000000000000000000, 0.000000000000000000, -1.000000000000000000 ) ) ;
#10243=DIRECTION ( 'NONE',  ( 0.000000000000000000, -0.000000000000000000, 1.000000000000000000 ) ) ;
#10244=EDGE_CURVE ( 'NONE', #1409, #9993, #20796, .T. ) ;
#10249=ADVANCED_FACE ( 'NONE', ( #123 ), #5373, .F. ) ;
#10260=PLANE ( 'NONE',  #12732 ) ;
#10266=AXIS2_PLACEMENT_3D ( 'NONE', #11325, #13181, #16839 ) ;
#10273=AXIS2_PLACEMENT_3D ( 'NONE', #16178, #1436, #14700 ) ;
#10283=CARTESIAN_POINT ( 'NONE',  ( -30.44534269664590553, 40.40463133211079594, 0.000000000000000000 ) ) ;
#10284=DIRECTION ( 'NONE',  ( 0.000000000000000000, 0.000000000000000000, -1.000000000000000000 ) ) ;
#10293=EDGE_LOOP ( 'NONE', ( #7553, #3701, #1692, #4598, #21414, #974, #14164, #24068, #8941, #22564, #9560, #9508, #16708, #5047, #21109, #17646, #15032, #3356, #12633, #7344, #8755, #11145, #11146, #10901, #21758, #273, #1050, #4593, #23404, #9113, #12839, #10858, #20969 ) ) ;
#10298=ORIENTED_EDGE ( 'NONE', *, *, #23354, .T. ) ;
#10301=DIRECTION ( 'NONE',  ( 1.000000000000000000, 2.600433232233976523E-16, -0.000000000000000000 ) ) ;
#10303=LINE ( 'NONE', #8479, #9126 ) ;
#10304=EDGE_CURVE ( 'NONE', #4131, #10954, #6318, .T. ) ;
#10314=VECTOR ( 'NONE', #10197, 1000.000000000000000 ) ;
#10316=AXIS2_PLACEMENT_3D ( 'NONE', #21424, #6170, #19107 ) ;
#10354=AXIS2_PLACEMENT_3D ( 'NONE', #15810, #21788, #21547 ) ;
#10365=EDGE_CURVE ( 'NONE', #1231, #16095, #13322, .T. ) ;
#10371=EDGE_LOOP ( 'NONE', ( #19765, #14195, #6294, #21117 ) ) ;
#10374=DIRECTION ( 'NONE',  ( 0.000000000000000000, 1.000000000000000000, 0.000000000000000000 ) ) ;
#10375=CARTESIAN_POINT ( 'NONE',  ( -40.29291594121673370, -26.62062637246459929, 11.00000000000000000 ) ) ;
#10380=ORIENTED_EDGE ( 'NONE', *, *, #11286, .T. ) ;
#10384=ORIENTED_EDGE ( 'NONE', *, *, #4465, .T. ) ;
#10389=DIRECTION ( 'NONE',  ( 0.000000000000000000, 0.000000000000000000, 1.000000000000000000 ) ) ;
#10391=AXIS2_PLACEMENT_3D ( 'NONE', #21130, #4436, #11851 ) ;
#10396=VERTEX_POINT ( 'NONE', #9969 ) ;
#10401=ORIENTED_EDGE ( 'NONE', *, *, #18146, .T. ) ;
#10402=ORIENTED_EDGE ( 'NONE', *, *, #12787, .F. ) ;
#10407=AXIS2_PLACEMENT_3D ( 'NONE', #12217, #15894, #8673 ) ;
#10429=CARTESIAN_POINT ( 'NONE',  ( -34.00000000000000000, -5.999999999999999112, 12.00000000000000000 ) ) ;
#10449=EDGE_CURVE ( 'NONE', #8760, #22901, #13768, .T. ) ;
#10453=AXIS2_PLACEMENT_3D ( 'NONE', #22236, #5506, #14882 ) ;
#10458=DIRECTION ( 'NONE',  ( -0.8247505806839237064, -0.5654966663575754504, 0.000000000000000000 ) ) ;
#10459=CIRCLE ( 'NONE', #12837, 20.85000000000000142 ) ;
#10462=LINE ( 'NONE', #23538, #15258 ) ;
#10465=ORIENTED_EDGE ( 'NONE', *, *, #23260, .T. ) ;
#10473=EDGE_CURVE ( 'NONE', #21725, #4506, #3204, .T. ) ;
#10474=ORIENTED_EDGE ( 'NONE', *, *, #7829, .F. ) ;
#10477=DIRECTION ( 'NONE',  ( -1.000000000000000000, 0.000000000000000000, 0.000000000000000000 ) ) ;
#10478=DIRECTION ( 'NONE',  ( 1.000000000000000000, 0.000000000000000000, -0.000000000000000000 ) ) ;
#10483=ORIENTED_EDGE ( 'NONE', *, *, #6050, .T. ) ;
#10485=DIRECTION ( 'NONE',  ( 1.000000000000000000, 0.000000000000000000, -0.000000000000000000 ) ) ;
#10486=DIRECTION ( 'NONE',  ( -0.000000000000000000, 0.000000000000000000, 1.000000000000000000 ) ) ;
#10487=( LENGTH_UNIT ( ) NAMED_UNIT ( * ) SI_UNIT ( .MILLI., .METRE. ) );
#10492=EDGE_CURVE ( 'NONE', #17642, #14945, #10462, .T. ) ;
#10498=ADVANCED_FACE ( 'NONE', ( #10569 ), #18034, .F. ) ;
#10500=ORIENTED_EDGE ( 'NONE', *, *, #5818, .T. ) ;
#10502=DIRECTION ( 'NONE',  ( 1.000000000000000000, 0.000000000000000000, 0.000000000000000000 ) ) ;
#10503=CYLINDRICAL_SURFACE ( 'NONE', #7970, 4.999999999999997335 ) ;
#10510=AXIS2_PLACEMENT_3D ( 'NONE', #639, #8048, #15492 ) ;
#10514=EDGE_LOOP ( 'NONE', ( #1306, #8386, #13679, #15646 ) ) ;
#10518=ORIENTED_EDGE ( 'NONE', *, *, #2996, .F. ) ;
#10522=CARTESIAN_POINT ( 'NONE',  ( -40.00000000000000000, 29.49999999999999645, 0.000000000000000000 ) ) ;
#10528=EDGE_LOOP ( 'NONE', ( #9977, #7473, #7259, #14539 ) ) ;
#10529=DIRECTION ( 'NONE',  ( -0.000000000000000000, -0.000000000000000000, -1.000000000000000000 ) ) ;
#10552=CARTESIAN_POINT ( 'NONE',  ( 40.00000000000000000, -29.49999999999999645, 11.00000000000000000 ) ) ;
#10559=DIRECTION ( 'NONE',  ( -0.1313947906041722513, -0.9913301211009810654, 0.000000000000000000 ) ) ;
#10560=CARTESIAN_POINT ( 'NONE',  ( -34.10000000000000142, -29.49999999999999645, 0.000000000000000000 ) ) ;
#10564=DIRECTION ( 'NONE',  ( -2.600433232233976523E-16, 1.000000000000000000, 0.000000000000000000 ) ) ;
#10569=FACE_OUTER_BOUND ( 'NONE', #20124, .T. ) ;
#10570=FACE_OUTER_BOUND ( 'NONE', #13114, .T. ) ;
#10575=FACE_OUTER_BOUND ( 'NONE', #7091, .T. ) ;
#10592=AXIS2_PLACEMENT_3D ( 'NONE', #8459, #6752, #6521 ) ;
#10593=AXIS2_PLACEMENT_3D ( 'NONE', #8570, #23821, #10755 ) ;
#10594=ORIENTED_EDGE ( 'NONE', *, *, #12940, .T. ) ;
#10600=( NAMED_UNIT ( * ) PLANE_ANGLE_UNIT ( ) SI_UNIT ( $, .RADIAN. ) );
#10602=LINE ( 'NONE', #21973, #13454 ) ;
#10615=DIRECTION ( 'NONE',  ( 1.000000000000000000, 8.320016671351592327E-16, 0.000000000000000000 ) ) ;
#10619=CARTESIAN_POINT ( 'NONE',  ( 0.000000000000000000, -45.00000000000000000, 3.000000000000002665 ) ) ;
#10623=EDGE_LOOP ( 'NONE', ( #8565, #15249, #4392, #20820 ) ) ;
#10628=EDGE_CURVE ( 'NONE', #7385, #5720, #21087, .T. ) ;
#10639=ORIENTED_EDGE ( 'NONE', *, *, #21834, .F. ) ;
#10646=AXIS2_PLACEMENT_3D ( 'NONE', #7339, #22240, #5406 ) ;
#10656=EDGE_CURVE ( 'NONE', #3076, #1666, #19535, .T. ) ;
#10665=DIRECTION ( 'NONE',  ( -0.000000000000000000, -0.000000000000000000, -1.000000000000000000 ) ) ;
#10666=CARTESIAN_POINT ( 'NONE',  ( -41.00000000000000000, -26.82133436441678853, 12.00000000000000000 ) ) ;
#10667=VECTOR ( 'NONE', #18674, 1000.000000000000000 ) ;
#10674=ORIENTED_EDGE ( 'NONE', *, *, #11367, .F. ) ;
#10676=EDGE_CURVE ( 'NONE', #8169, #7597, #10168, .T. ) ;
#10680=CARTESIAN_POINT ( 'NONE',  ( 42.00000000000000000, 3.999999999999987121, 8.500000000000000000 ) ) ;
#10698=DIRECTION ( 'NONE',  ( -0.000000000000000000, -0.000000000000000000, -1.000000000000000000 ) ) ;
#10700=CARTESIAN_POINT ( 'NONE',  ( 37.00000000000000711, -29.50000000000000355, 11.50000000000000000 ) ) ;
#10717=CIRCLE ( 'NONE', #9537, 8.000000000000003553 ) ;
#10718=DIRECTION ( 'NONE',  ( -0.000000000000000000, -0.000000000000000000, -1.000000000000000000 ) ) ;
#10721=DIRECTION ( 'NONE',  ( 0.000000000000000000, 0.000000000000000000, 1.000000000000000000 ) ) ;
#10727=VECTOR ( 'NONE', #10100, 1000.000000000000000 ) ;
#10732=DIRECTION ( 'NONE',  ( -0.000000000000000000, -0.000000000000000000, 1.000000000000000000 ) ) ;
#10733=VERTEX_POINT ( 'NONE', #16677 ) ;
#10738=EDGE_CURVE ( 'NONE', #7598, #20616, #8975, .T. ) ;
#10740=VECTOR ( 'NONE', #3856, 1000.000000000000000 ) ;
#10741=EDGE_CURVE ( 'NONE', #12778, #9530, #9759, .T. ) ;
#10742=AXIS2_PLACEMENT_3D ( 'NONE', #19523, #2803, #6339 ) ;
#10743=CARTESIAN_POINT ( 'NONE',  ( -41.00000000000000000, 5.000000000000000888, 11.00000000000000000 ) ) ;
#10755=DIRECTION ( 'NONE',  ( 1.000000000000000000, 0.000000000000000000, 0.000000000000000000 ) ) ;
#10759=ORIENTED_EDGE ( 'NONE', *, *, #23736, .F. ) ;
#10763=AXIS2_PLACEMENT_3D ( 'NONE', #2433, #22828, #6103 ) ;
#10764=CYLINDRICAL_SURFACE ( 'NONE', #5118, 1.000000000000000000 ) ;
#10781=DIRECTION ( 'NONE',  ( -0.8757121056631640421, -0.4828336235133042775, 0.000000000000000000 ) ) ;
#10795=ORIENTED_EDGE ( 'NONE', *, *, #6926, .F. ) ;
#10799=AXIS2_PLACEMENT_3D ( 'NONE', #300, #11490, #18963 ) ;
#10803=AXIS2_PLACEMENT_3D ( 'NONE', #23657, #12508, #7032 ) ;
#10816=FACE_OUTER_BOUND ( 'NONE', #17110, .T. ) ;
#10817=ORIENTED_EDGE ( 'NONE', *, *, #19994, .T. ) ;
#10823=EDGE_CURVE ( 'NONE', #8265, #5826, #17404, .T. ) ;
#10840=DIRECTION ( 'NONE',  ( 1.000000000000000000, 0.000000000000000000, 0.000000000000000000 ) ) ;
#10841=CARTESIAN_POINT ( 'NONE',  ( -27.70933665152130843, -40.41277845351217479, 12.00000000000000000 ) ) ;
#10842=ORIENTED_EDGE ( 'NONE', *, *, #17214, .F. ) ;
#10845=ORIENTED_EDGE ( 'NONE', *, *, #9462, .T. ) ;
#10846=CARTESIAN_POINT ( 'NONE',  ( 29.00000000000000000, 29.50000000000000355, 11.50000000000000000 ) ) ;
#10847=CARTESIAN_POINT ( 'NONE',  ( 2.454813078130514813E-15, 16.67999999999999972, 12.00000000000000000 ) ) ;
#10850=FACE_OUTER_BOUND ( 'NONE', #22407, .T. ) ;
#10851=CARTESIAN_POINT ( 'NONE',  ( 29.00000000000000000, -29.50000000000000355, 12.00000000000000000 ) ) ;
#10858=ORIENTED_EDGE ( 'NONE', *, *, #2974, .T. ) ;
#10866=FACE_OUTER_BOUND ( 'NONE', #6526, .T. ) ;
#10878=ORIENTED_EDGE ( 'NONE', *, *, #16508, .T. ) ;
#10883=EDGE_LOOP ( 'NONE', ( #12657, #13766, #23500, #21408 ) ) ;
#10885=DIRECTION ( 'NONE',  ( 0.000000000000000000, -0.000000000000000000, -1.000000000000000000 ) ) ;
#10887=ADVANCED_FACE ( 'NONE', ( #17774 ), #21679, .T. ) ;
#10888=ADVANCED_FACE ( 'NONE', ( #19735 ), #3014, .F. ) ;
#10889=DIRECTION ( 'NONE',  ( 1.000000000000000000, 0.000000000000000000, 0.000000000000000000 ) ) ;
#10901=ORIENTED_EDGE ( 'NONE', *, *, #6153, .T. ) ;
#10906=CIRCLE ( 'NONE', #418, 1.500000000000001332 ) ;
#10915=DIRECTION ( 'NONE',  ( -1.000000000000000000, -2.600433232233976523E-16, 0.000000000000000000 ) ) ;
#10921=ORIENTED_EDGE ( 'NONE', *, *, #16821, .F. ) ;
#10922=ORIENTED_EDGE ( 'NONE', *, *, #15110, .T. ) ;
#10938=ORIENTED_EDGE ( 'NONE', *, *, #16506, .T. ) ;
#10945=CIRCLE ( 'NONE', #81, 4.999999999999997335 ) ;
#10952=ORIENTED_EDGE ( 'NONE', *, *, #12393, .F. ) ;
#10954=VERTEX_POINT ( 'NONE', #4723 ) ;
#10968=EDGE_CURVE ( 'NONE', #21802, #8229, #10945, .T. ) ;
#10970=CIRCLE ( 'NONE', #22298, 1.000000000000000888 ) ;
#10979=VECTOR ( 'NONE', #13073, 1000.000000000000000 ) ;
#10982=DIRECTION ( 'NONE',  ( 0.000000000000000000, 0.000000000000000000, 1.000000000000000000 ) ) ;
#10992=AXIS2_PLACEMENT_3D ( 'NONE', #15806, #8585, #4713 ) ;
#10997=CARTESIAN_POINT ( 'NONE',  ( -40.29291594121673370, 26.62062637246459929, 11.00000000000000000 ) ) ;
#10998=EDGE_CURVE ( 'NONE', #21352, #411, #7361, .T. ) ;
#11006=DIRECTION ( 'NONE',  ( 0.000000000000000000, 0.000000000000000000, -1.000000000000000000 ) ) ;
#11011=LINE ( 'NONE', #15046, #23922 ) ;
#11014=AXIS2_PLACEMENT_3D ( 'NONE', #6639, #21522, #12234 ) ;
#11023=CYLINDRICAL_SURFACE ( 'NONE', #10097, 1.000000000000002442 ) ;
#11029=ADVANCED_FACE ( 'NONE', ( #24084 ), #1646, .T. ) ;
#11030=ORIENTED_EDGE ( 'NONE', *, *, #13568, .F. ) ;
#11051=VERTEX_POINT ( 'NONE', #20199 ) ;
#11064=PLANE ( 'NONE',  #452 ) ;
#11068=VECTOR ( 'NONE', #19287, 1000.000000000000000 ) ;
#11069=AXIS2_PLACEMENT_3D ( 'NONE', #12974, #3950, #3589 ) ;
#11091=ORIENTED_EDGE ( 'NONE', *, *, #20894, .T. ) ;
#11095=DIRECTION ( 'NONE',  ( 1.000000000000000000, 0.000000000000000000, 0.000000000000000000 ) ) ;
#11099=AXIS2_PLACEMENT_3D ( 'NONE', #20503, #17176, #7538 ) ;
#11103=ADVANCED_FACE ( 'NONE', ( #18605 ), #1884, .T. ) ;
#11105=ORIENTED_EDGE ( 'NONE', *, *, #19783, .T. ) ;
#11134=EDGE_LOOP ( 'NONE', ( #6250, #7435, #21783, #18424 ) ) ;
#11145=ORIENTED_EDGE ( 'NONE', *, *, #15607, .T. ) ;
#11146=ORIENTED_EDGE ( 'NONE', *, *, #12996, .T. ) ;
#11151=DIRECTION ( 'NONE',  ( -1.000000000000000000, 2.600433232233976523E-16, 0.000000000000000000 ) ) ;
#11163=DIRECTION ( 'NONE',  ( 0.000000000000000000, 0.000000000000000000, -1.000000000000000000 ) ) ;
#11167=VERTEX_POINT ( 'NONE', #5786 ) ;
#11172=VERTEX_POINT ( 'NONE', #17000 ) ;
#11177=FACE_OUTER_BOUND ( 'NONE', #11412, .T. ) ;
#11184=CARTESIAN_POINT ( 'NONE',  ( -41.50000000000000000, 28.80990663662250739, 12.00000000000000000 ) ) ;
#11186=CARTESIAN_POINT ( 'NONE',  ( -41.00000000000000000, -3.851859888774471706E-31, 8.500000000000000000 ) ) ;
#11189=VERTEX_POINT ( 'NONE', #13463 ) ;
#11198=ORIENTED_EDGE ( 'NONE', *, *, #16613, .F. ) ;
#11200=DIRECTION ( 'NONE',  ( -0.000000000000000000, -0.000000000000000000, 1.000000000000000000 ) ) ;
#11201=AXIS2_PLACEMENT_3D ( 'NONE', #13459, #7707, #14796 ) ;
#11206=EDGE_CURVE ( 'NONE', #671, #8434, #18768, .T. ) ;
#11213=ADVANCED_FACE ( 'NONE', ( #7711, #15147 ), #22616, .T. ) ;
#11218=CARTESIAN_POINT ( 'NONE',  ( -21.13207267780287069, 38.32709852940855910, 0.000000000000000000 ) ) ;
#11219=DIRECTION ( 'NONE',  ( -0.000000000000000000, 0.000000000000000000, 1.000000000000000000 ) ) ;
#11221=VERTEX_POINT ( 'NONE', #15405 ) ;
#11228=EDGE_LOOP ( 'NONE', ( #5024, #11934, #17560, #6408 ) ) ;
#11231=FACE_OUTER_BOUND ( 'NONE', #3388, .T. ) ;
#11245=EDGE_LOOP ( 'NONE', ( #18844, #276, #9781, #10401, #17608, #12596, #8421, #10127, #8794, #21840, #18203, #9554, #18532, #13448, #5721, #11990, #5782, #17005, #23899, #16630, #53, #12874, #22375, #15451 ) ) ;
#11256=ORIENTED_EDGE ( 'NONE', *, *, #19600, .F. ) ;
#11259=VERTEX_POINT ( 'NONE', #13834 ) ;
#11262=PLANE ( 'NONE',  #22535 ) ;
#11275=CARTESIAN_POINT ( 'NONE',  ( 33.99999999999998579, -1.387778780781445676E-14, 10.49999999999999822 ) ) ;
#11279=ORIENTED_EDGE ( 'NONE', *, *, #2757, .T. ) ;
#11281=( NAMED_UNIT ( * ) SI_UNIT ( $, .STERADIAN. ) SOLID_ANGLE_UNIT ( ) );
#11282=DIRECTION ( 'NONE',  ( 1.000000000000000000, 0.000000000000000000, 0.000000000000000000 ) ) ;
#11286=EDGE_CURVE ( 'NONE', #18239, #16829, #8644, .T. ) ;
#11290=CYLINDRICAL_SURFACE ( 'NONE', #21956, 1.000000000000000888 ) ;
#11291=EDGE_CURVE ( 'NONE', #16095, #1231, #12540, .T. ) ;
#11301=DIRECTION ( 'NONE',  ( -0.000000000000000000, -0.000000000000000000, -1.000000000000000000 ) ) ;
#11309=EDGE_LOOP ( 'NONE', ( #17782, #1912, #12237, #887 ) ) ;
#11310=CARTESIAN_POINT ( 'NONE',  ( 39.00000000000000000, 29.49999999999999645, 12.00000000000000000 ) ) ;
#11312=PLANE ( 'NONE',  #10224 ) ;
#11318=CARTESIAN_POINT ( 'NONE',  ( 29.00000000000000000, -29.50000000000000355, 11.50000000000000000 ) ) ;
#11322=FACE_OUTER_BOUND ( 'NONE', #6179, .T. ) ;
#11325=CARTESIAN_POINT ( 'NONE',  ( 29.00000000000000000, 29.50000000000000355, 11.50000000000000000 ) ) ;
#11327=CIRCLE ( 'NONE', #2413, 4.000000000000000000 ) ;
#11328=ORIENTED_EDGE ( 'NONE', *, *, #6578, .F. ) ;
#11330=PLANE ( 'NONE',  #20364 ) ;
#11356=DIRECTION ( 'NONE',  ( -0.000000000000000000, 0.000000000000000000, 1.000000000000000000 ) ) ;
#11362=CARTESIAN_POINT ( 'NONE',  ( 28.27483331787888332, -41.23752903419610050, 11.00000000000000000 ) ) ;
#11363=DIRECTION ( 'NONE',  ( -1.000000000000000000, 0.000000000000000000, 0.000000000000000000 ) ) ;
#11367=EDGE_CURVE ( 'NONE', #7050, #21802, #16446, .T. ) ;
#11372=VECTOR ( 'NONE', #22667, 1000.000000000000000 ) ;
#11379=EDGE_CURVE ( 'NONE', #3226, #20146, #15245, .T. ) ;
#11380=CARTESIAN_POINT ( 'NONE',  ( -34.00000000000000000, -3.999999999999999112, 9.500000000000000000 ) ) ;
#11387=DIRECTION ( 'NONE',  ( -0.000000000000000000, -0.000000000000000000, -1.000000000000000000 ) ) ;
#11390=DIRECTION ( 'NONE',  ( -1.000000000000000000, -0.000000000000000000, -0.000000000000000000 ) ) ;
#11412=EDGE_LOOP ( 'NONE', ( #791, #2704, #13599, #10157 ) ) ;
#11422=VECTOR ( 'NONE', #6183, 1000.000000000000000 ) ;
#11444=CARTESIAN_POINT ( 'NONE',  ( -41.50000000000000000, -28.80990663662250739, 11.00000000000000000 ) ) ;
#11453=AXIS2_PLACEMENT_3D ( 'NONE', #19801, #12688, #20154 ) ;
#11486=VECTOR ( 'NONE', #7523, 1000.000000000000000 ) ;
#11490=DIRECTION ( 'NONE',  ( -0.000000000000000000, -0.000000000000000000, -1.000000000000000000 ) ) ;
#11492=VERTEX_POINT ( 'NONE', #7912 ) ;
#11494=FACE_BOUND ( 'NONE', #11569, .T. ) ;
#11515=DIRECTION ( 'NONE',  ( 1.000000000000000000, 4.625929269271481378E-15, 0.000000000000000000 ) ) ;
#11520=ORIENTED_EDGE ( 'NONE', *, *, #20776, .T. ) ;
#11538=ADVANCED_FACE ( 'NONE', ( #15111 ), #22576, .F. ) ;
#11560=DIRECTION ( 'NONE',  ( 1.000000000000000000, 2.600433232233976523E-16, -0.000000000000000000 ) ) ;
#11569=EDGE_LOOP ( 'NONE', ( #20677, #9920 ) ) ;
#11580=ORIENTED_EDGE ( 'NONE', *, *, #20610, .T. ) ;
#11583=CARTESIAN_POINT ( 'NONE',  ( 29.00000000000000000, 29.50000000000000355, 0.000000000000000000 ) ) ;
#11589=CARTESIAN_POINT ( 'NONE',  ( -31.10231664966676846, 45.36128193761570770, 0.000000000000000000 ) ) ;
#11593=CARTESIAN_POINT ( 'NONE',  ( -34.00000000000000000, -3.851859888774471706E-31, 11.00000000000000000 ) ) ;
#11595=DIRECTION ( 'NONE',  ( -0.8757121056631642642, 0.4828336235133042220, 0.000000000000000000 ) ) ;
#11596=DIRECTION ( 'NONE',  ( -1.000000000000000000, 0.000000000000000000, 0.000000000000000000 ) ) ;
#11606=CARTESIAN_POINT ( 'NONE',  ( -19.84999999999999787, 16.67999999999985405, 13.50000000000000178 ) ) ;
#11615=FACE_BOUND ( 'NONE', #1873, .T. ) ;
#11616=CARTESIAN_POINT ( 'NONE',  ( 29.00000000000000000, 29.50000000000000355, 11.50000000000000000 ) ) ;
#11617=DIRECTION ( 'NONE',  ( -0.000000000000000000, -0.000000000000000000, -1.000000000000000000 ) ) ;
#11638=FACE_OUTER_BOUND ( 'NONE', #23127, .T. ) ;
#11645=CARTESIAN_POINT ( 'NONE',  ( 42.00000000000000000, 0.000000000000000000, 11.00000000000000000 ) ) ;
#11646=CYLINDRICAL_SURFACE ( 'NONE', #6807, 5.099999999999996980 ) ;
#11648=CARTESIAN_POINT ( 'NONE',  ( -40.00000000000000000, 0.000000000000000000, 11.00000000000000000 ) ) ;
#11664=CARTESIAN_POINT ( 'NONE',  ( -40.77574956473004164, 27.49633847812775755, 12.00000000000000000 ) ) ;
#11666=CYLINDRICAL_SURFACE ( 'NONE', #8364, 50.00000000000000000 ) ;
#11668=DIRECTION ( 'NONE',  ( 1.000000000000000000, 0.000000000000000000, 0.000000000000000000 ) ) ;
#11674=ORIENTED_EDGE ( 'NONE', *, *, #6470, .T. ) ;
#11685=DIRECTION ( 'NONE',  ( 0.000000000000000000, -0.000000000000000000, -1.000000000000000000 ) ) ;
#11694=FACE_OUTER_BOUND ( 'NONE', #23441, .T. ) ;
#11710=AXIS2_PLACEMENT_3D ( 'NONE', #24007, #18745, #20116 ) ;
#11712=EDGE_LOOP ( 'NONE', ( #10384, #9241, #21667, #2751 ) ) ;
#11714=ADVANCED_FACE ( 'NONE', ( #21728 ), #12187, .F. ) ;
#11716=ORIENTED_EDGE ( 'NONE', *, *, #10473, .T. ) ;
#11718=CARTESIAN_POINT ( 'NONE',  ( 42.00000000000000000, -6.000000000000015099, 11.00000000000000000 ) ) ;
#11723=VERTEX_POINT ( 'NONE', #20139 ) ;
#11732=ORIENTED_EDGE ( 'NONE', *, *, #11286, .F. ) ;
#11733=ORIENTED_EDGE ( 'NONE', *, *, #10968, .F. ) ;
#11748=AXIS2_PLACEMENT_3D ( 'NONE', #22159, #14800, #11006 ) ;
#11783=AXIS2_PLACEMENT_3D ( 'NONE', #18243, #12488, #14564 ) ;
#11789=AXIS2_PLACEMENT_3D ( 'NONE', #17958, #7074, #23454 ) ;
#11794=AXIS2_PLACEMENT_3D ( 'NONE', #8999, #9346, #16795 ) ;
#11800=ORIENTED_EDGE ( 'NONE', *, *, #20597, .F. ) ;
#11811=CIRCLE ( 'NONE', #10646, 50.00000000000000000 ) ;
#11813=AXIS2_PLACEMENT_3D ( 'NONE', #2125, #7364, #20564 ) ;
#11816=CARTESIAN_POINT ( 'NONE',  ( -40.77574956473004164, 27.49633847812775755, 0.000000000000000000 ) ) ;
#11819=ORIENTED_EDGE ( 'NONE', *, *, #3786, .T. ) ;
#11830=FACE_OUTER_BOUND ( 'NONE', #22926, .T. ) ;
#11841=DIRECTION ( 'NONE',  ( -1.000000000000000000, 0.000000000000000000, 0.000000000000000000 ) ) ;
#11845=CARTESIAN_POINT ( 'NONE',  ( -21.13207267780287069, -38.32709852940855910, 12.00000000000000000 ) ) ;
#11848=AXIS2_PLACEMENT_3D ( 'NONE', #9805, #22428, #3754 ) ;
#11851=DIRECTION ( 'NONE',  ( 1.000000000000000000, -1.776356839400250465E-15, 0.000000000000000000 ) ) ;
#11854=VERTEX_POINT ( 'NONE', #9001 ) ;
#11856=CARTESIAN_POINT ( 'NONE',  ( 0.000000000000000000, 0.000000000000000000, 12.00000000000000000 ) ) ;
#11863=FACE_OUTER_BOUND ( 'NONE', #11245, .T. ) ;
#11872=CARTESIAN_POINT ( 'NONE',  ( 42.00000000000000000, 3.999999999999987121, 10.49999999999999822 ) ) ;
#11874=EDGE_CURVE ( 'NONE', #3246, #7962, #20360, .T. ) ;
#11894=VECTOR ( 'NONE', #5752, 1000.000000000000000 ) ;
#11898=AXIS2_PLACEMENT_3D ( 'NONE', #12361, #14077, #13842 ) ;
#11907=EDGE_LOOP ( 'NONE', ( #20348, #18711 ) ) ;
#11913=AXIS2_PLACEMENT_3D ( 'NONE', #10226, #3057, #10477 ) ;
#11916=CYLINDRICAL_SURFACE ( 'NONE', #627, 11.00000000000000711 ) ;
#11919=DIRECTION ( 'NONE',  ( 0.000000000000000000, 1.000000000000000000, 0.000000000000000000 ) ) ;
#11921=ADVANCED_FACE ( 'NONE', ( #5602 ), #1660, .F. ) ;
#11925=DIRECTION ( 'NONE',  ( 0.000000000000000000, 0.000000000000000000, -1.000000000000000000 ) ) ;
#11933=AXIS2_PLACEMENT_3D ( 'NONE', #22947, #5981, #2319 ) ;
#11934=ORIENTED_EDGE ( 'NONE', *, *, #6741, .T. ) ;
#11942=CIRCLE ( 'NONE', #17803, 4.999999999999997335 ) ;
#11948=EDGE_CURVE ( 'NONE', #12416, #16460, #13977, .T. ) ;
#11949=EDGE_CURVE ( 'NONE', #1117, #8434, #16073, .T. ) ;
#11964=DIRECTION ( 'NONE',  ( 0.8757121056631640421, -0.4828336235133042775, 0.000000000000000000 ) ) ;
#11977=ORIENTED_EDGE ( 'NONE', *, *, #15791, .T. ) ;
#11980=CARTESIAN_POINT ( 'NONE',  ( 40.00000000000000000, 28.80990663662251450, 12.00000000000000000 ) ) ;
#11981=CARTESIAN_POINT ( 'NONE',  ( 20.85000000000000497, -16.67999999999999972, 13.50000000000000178 ) ) ;
#11988=ORIENTED_EDGE ( 'NONE', *, *, #14081, .F. ) ;
#11990=ORIENTED_EDGE ( 'NONE', *, *, #6826, .T. ) ;
#11991=EDGE_CURVE ( 'NONE', #19009, #9993, #20607, .T. ) ;
#11998=FACE_OUTER_BOUND ( 'NONE', #21691, .T. ) ;
#12004=EDGE_CURVE ( 'NONE', #15840, #4885, #9713, .T. ) ;
#12032=ADVANCED_FACE ( 'NONE', ( #6417 ), #897, .F. ) ;
#12038=CARTESIAN_POINT ( 'NONE',  ( 40.00000000000000000, -29.49999999999999645, 12.00000000000000000 ) ) ;
#12043=ORIENTED_EDGE ( 'NONE', *, *, #6741, .F. ) ;
#12049=CARTESIAN_POINT ( 'NONE',  ( 42.00000000000000000, 26.82133436441678853, 11.00000000000000000 ) ) ;
#12050=CIRCLE ( 'NONE', #8548, 5.099999999999996980 ) ;
#12052=ADVANCED_FACE ( 'NONE', ( #11998 ), #11290, .T. ) ;
#12061=CARTESIAN_POINT ( 'NONE',  ( 41.00000000000000000, -6.000000000000015099, 9.500000000000000000 ) ) ;
#12064=CARTESIAN_POINT ( 'NONE',  ( -29.00000000000000000, -29.49999999999999645, 0.000000000000000000 ) ) ;
#12066=DIRECTION ( 'NONE',  ( -1.000000000000000000, -0.000000000000000000, 0.000000000000000000 ) ) ;
#12069=VERTEX_POINT ( 'NONE', #12607 ) ;
#12072=DIRECTION ( 'NONE',  ( 1.000000000000000000, 0.000000000000000000, 0.000000000000000000 ) ) ;
#12076=LINE ( 'NONE', #19549, #8338 ) ;
#12095=LINE ( 'NONE', #6396, #1384 ) ;
#12099=CARTESIAN_POINT ( 'NONE',  ( -34.00000000000000000, 5.999999999999999112, 12.00000000000000000 ) ) ;
#12103=EDGE_LOOP ( 'NONE', ( #19722, #16424, #14960, #9393 ) ) ;
#12104=ADVANCED_FACE ( 'NONE', ( #9064 ), #4812, .T. ) ;
#12111=CARTESIAN_POINT ( 'NONE',  ( -21.84999999999999787, 16.67999999999985405, 12.00000000000000000 ) ) ;
#12113=VECTOR ( 'NONE', #18009, 1000.000000000000000 ) ;
#12121=VERTEX_POINT ( 'NONE', #21543 ) ;
#12132=ADVANCED_FACE ( 'NONE', ( #6653 ), #21782, .F. ) ;
#12134=ORIENTED_EDGE ( 'NONE', *, *, #15234, .F. ) ;
#12135=ORIENTED_EDGE ( 'NONE', *, *, #21700, .T. ) ;
#12138=ADVANCED_FACE ( 'NONE', ( #14200 ), #14558, .T. ) ;
#12140=ADVANCED_FACE ( 'NONE', ( #5305 ), #16859, .F. ) ;
#12145=ORIENTED_EDGE ( 'NONE', *, *, #12749, .T. ) ;
#12154=AXIS2_PLACEMENT_3D ( 'NONE', #8441, #3079, #10502 ) ;
#12157=DIRECTION ( 'NONE',  ( -0.000000000000000000, -0.000000000000000000, -1.000000000000000000 ) ) ;
#12163=EDGE_CURVE ( 'NONE', #8481, #1117, #18055, .T. ) ;
#12181=CIRCLE ( 'NONE', #18429, 11.00000000000000711 ) ;
#12185=TOROIDAL_SURFACE ( 'NONE', #121, 10.00000000000000533, 1.000000000000000000 ) ;
#12186=DIRECTION ( 'NONE',  ( 0.8757121056631640421, 0.4828336235133042775, 0.000000000000000000 ) ) ;
#12187=CYLINDRICAL_SURFACE ( 'NONE', #19193, 5.099999999999996980 ) ;
#12188=AXIS2_PLACEMENT_3D ( 'NONE', #13717, #23811, #16249 ) ;
#12189=VERTEX_POINT ( 'NONE', #20298 ) ;
#12200=AXIS2_PLACEMENT_3D ( 'NONE', #16161, #14319, #17992 ) ;
#12206=AXIS2_PLACEMENT_3D ( 'NONE', #18585, #18941, #3922 ) ;
#12212=DIRECTION ( 'NONE',  ( -0.000000000000000000, -0.000000000000000000, -1.000000000000000000 ) ) ;
#12217=CARTESIAN_POINT ( 'NONE',  ( 33.99999999999998579, -6.000000000000013323, 11.00000000000000000 ) ) ;
#12218=CIRCLE ( 'NONE', #8699, 1.000000000000001998 ) ;
#12220=CIRCLE ( 'NONE', #17685, 1.000000000000000000 ) ;
#12234=DIRECTION ( 'NONE',  ( 0.000000000000000000, 0.000000000000000000, -1.000000000000000000 ) ) ;
#12235=ADVANCED_FACE ( 'NONE', ( #22150 ), #14908, .T. ) ;
#12237=ORIENTED_EDGE ( 'NONE', *, *, #9315, .T. ) ;
#12259=CIRCLE ( 'NONE', #1749, 8.000000000000003553 ) ;
#12264=DIRECTION ( 'NONE',  ( -0.000000000000000000, -0.000000000000000000, -1.000000000000000000 ) ) ;
#12269=AXIS2_PLACEMENT_3D ( 'NONE', #22409, #22172, #18151 ) ;
#12285=CARTESIAN_POINT ( 'NONE',  ( -20.99999999999999645, 29.49999999999999645, 11.50000000000000000 ) ) ;
#12288=CIRCLE ( 'NONE', #1778, 5.099999999999996980 ) ;
#12301=VERTEX_POINT ( 'NONE', #9539 ) ;
#12314=DIRECTION ( 'NONE',  ( -0.000000000000000000, -0.000000000000000000, -1.000000000000000000 ) ) ;
#12322=EDGE_CURVE ( 'NONE', #22129, #13339, #3937, .T. ) ;
#12327=CIRCLE ( 'NONE', #1821, 5.099999999999996980 ) ;
#12333=DIRECTION ( 'NONE',  ( 1.000000000000000000, 0.000000000000000000, 0.000000000000000000 ) ) ;
#12342=CARTESIAN_POINT ( 'NONE',  ( -23.90000000000000213, -29.49999999999999645, 0.000000000000000000 ) ) ;
#12351=ADVANCED_FACE ( 'NONE', ( #21032 ), #13465, .T. ) ;
#12361=CARTESIAN_POINT ( 'NONE',  ( -42.00000000000000000, 4.000000000000000888, 10.49999999999999822 ) ) ;
#12364=EDGE_CURVE ( 'NONE', #5671, #22129, #20781, .T. ) ;
#12372=DIRECTION ( 'NONE',  ( -0.000000000000000000, -0.000000000000000000, -1.000000000000000000 ) ) ;
#12373=VERTEX_POINT ( 'NONE', #20668 ) ;
#12381=ORIENTED_EDGE ( 'NONE', *, *, #684, .F. ) ;
#12386=DIRECTION ( 'NONE',  ( 0.000000000000000000, 0.000000000000000000, 1.000000000000000000 ) ) ;
#12389=DIRECTION ( 'NONE',  ( -1.000000000000000000, 0.000000000000000000, 0.000000000000000000 ) ) ;
#12393=EDGE_CURVE ( 'NONE', #5011, #22408, #15407, .T. ) ;
#12396=ORIENTED_EDGE ( 'NONE', *, *, #20182, .F. ) ;
#12398=EDGE_CURVE ( 'NONE', #9485, #3124, #4082, .T. ) ;
#12406=CARTESIAN_POINT ( 'NONE',  ( 33.99999999999998579, 4.999999999999985789, 11.00000000000000000 ) ) ;
#12416=VERTEX_POINT ( 'NONE', #669 ) ;
#12417=CARTESIAN_POINT ( 'NONE',  ( 41.50000000000000000, 28.80990663662250739, 0.000000000000000000 ) ) ;
#12426=EDGE_CURVE ( 'NONE', #17472, #1813, #540, .T. ) ;
#12436=CARTESIAN_POINT ( 'NONE',  ( 41.00000000000000000, -6.000000000000015099, 11.00000000000000000 ) ) ;
#12453=DIRECTION ( 'NONE',  ( -0.000000000000000000, -0.000000000000000000, -1.000000000000000000 ) ) ;
#12461=DIRECTION ( 'NONE',  ( 1.000000000000000000, 0.000000000000000000, 0.000000000000000000 ) ) ;
#12463=LINE ( 'NONE', #19817, #9257 ) ;
#12464=ORIENTED_EDGE ( 'NONE', *, *, #4858, .T. ) ;
#12465=CARTESIAN_POINT ( 'NONE',  ( -29.00000000000000000, 29.49999999999999645, 11.00000000000000000 ) ) ;
#12467=DIRECTION ( 'NONE',  ( 1.000000000000000000, 0.000000000000000000, 0.000000000000000000 ) ) ;
#12476=EDGE_CURVE ( 'NONE', #15840, #666, #18845, .T. ) ;
#12484=DIRECTION ( 'NONE',  ( 1.000000000000000000, 0.000000000000000000, 0.000000000000000000 ) ) ;
#12488=DIRECTION ( 'NONE',  ( 0.000000000000000000, -0.000000000000000000, -1.000000000000000000 ) ) ;
#12491=DIRECTION ( 'NONE',  ( 1.000000000000000000, 0.000000000000000000, -0.000000000000000000 ) ) ;
#12498=EDGE_CURVE ( 'NONE', #11723, #8481, #12218, .T. ) ;
#12500=AXIS2_PLACEMENT_3D ( 'NONE', #8422, #10374, #21613 ) ;
#12508=DIRECTION ( 'NONE',  ( 0.000000000000000000, -1.000000000000000000, 0.000000000000000000 ) ) ;
#12509=CARTESIAN_POINT ( 'NONE',  ( -19.84999999999999787, 16.67999999999985405, 14.50000000000000000 ) ) ;
#12525=EDGE_CURVE ( 'NONE', #145, #19949, #2616, .T. ) ;
#12540=CIRCLE ( 'NONE', #3986, 8.000000000000003553 ) ;
#12541=AXIS2_PLACEMENT_3D ( 'NONE', #15148, #13332, #18357 ) ;
#12543=AXIS2_PLACEMENT_3D ( 'NONE', #3813, #7691, #1966 ) ;
#12545=DIRECTION ( 'NONE',  ( 1.000000000000000000, 2.600433232233976523E-16, -0.000000000000000000 ) ) ;
#12552=ORIENTED_EDGE ( 'NONE', *, *, #3348, .F. ) ;
#12557=AXIS2_PLACEMENT_3D ( 'NONE', #15353, #140, #14866 ) ;
#12562=CARTESIAN_POINT ( 'NONE',  ( -2.024999999999999911, -45.00000000000000000, 0.000000000000000000 ) ) ;
#12581=VECTOR ( 'NONE', #12773, 1000.000000000000000 ) ;
#12586=AXIS2_PLACEMENT_3D ( 'NONE', #4770, #8415, #16097 ) ;
#12594=DIRECTION ( 'NONE',  ( 0.000000000000000000, -1.000000000000000000, 0.000000000000000000 ) ) ;
#12596=ORIENTED_EDGE ( 'NONE', *, *, #15911, .F. ) ;
#12607=CARTESIAN_POINT ( 'NONE',  ( -34.00000000000000000, 5.999999999999999112, 12.00000000000000000 ) ) ;
#12624=DIRECTION ( 'NONE',  ( -0.000000000000000000, -0.000000000000000000, -1.000000000000000000 ) ) ;
#12631=LINE ( 'NONE', #1663, #17935 ) ;
#12632=VERTEX_POINT ( 'NONE', #10283 ) ;
#12633=ORIENTED_EDGE ( 'NONE', *, *, #24097, .T. ) ;
#12641=AXIS2_PLACEMENT_3D ( 'NONE', #4854, #6669, #19738 ) ;
#12648=ADVANCED_FACE ( 'NONE', ( #15906 ), #23370, .T. ) ;
#12649=CARTESIAN_POINT ( 'NONE',  ( -41.00000000000000000, -6.000000000000000888, 11.00000000000000000 ) ) ;
#12656=FACE_OUTER_BOUND ( 'NONE', #16081, .T. ) ;
#12657=ORIENTED_EDGE ( 'NONE', *, *, #20814, .F. ) ;
#12658=EDGE_LOOP ( 'NONE', ( #5262, #4761, #18727, #4469 ) ) ;
#12677=CIRCLE ( 'NONE', #10407, 1.000000000000000888 ) ;
#12679=CARTESIAN_POINT ( 'NONE',  ( -30.44534269664590553, -40.40463133211081015, 11.00000000000000000 ) ) ;
#12688=DIRECTION ( 'NONE',  ( -0.000000000000000000, -0.000000000000000000, 1.000000000000000000 ) ) ;
#12690=CARTESIAN_POINT ( 'NONE',  ( 21.13207267780287069, 38.32709852940855910, 11.00000000000000000 ) ) ;
#12695=DIRECTION ( 'NONE',  ( -0.000000000000000000, -0.000000000000000000, -1.000000000000000000 ) ) ;
#12711=DIRECTION ( 'NONE',  ( 1.000000000000000000, 0.000000000000000000, 0.000000000000000000 ) ) ;
#12718=ORIENTED_EDGE ( 'NONE', *, *, #4574, .F. ) ;
#12729=ORIENTED_EDGE ( 'NONE', *, *, #12476, .T. ) ;
#12732=AXIS2_PLACEMENT_3D ( 'NONE', #11845, #17714, #11964 ) ;
#12734=DIRECTION ( 'NONE',  ( 0.000000000000000000, 1.000000000000000000, 0.000000000000000000 ) ) ;
#12736=EDGE_LOOP ( 'NONE', ( #14338, #21178, #17748, #8341 ) ) ;
#12743=DIRECTION ( 'NONE',  ( 0.000000000000000000, -1.000000000000000000, 0.000000000000000000 ) ) ;
#12745=FACE_OUTER_BOUND ( 'NONE', #13462, .T. ) ;
#12749=EDGE_CURVE ( 'NONE', #3260, #4159, #4042, .T. ) ;
#12754=ORIENTED_EDGE ( 'NONE', *, *, #15110, .F. ) ;
#12758=EDGE_CURVE ( 'NONE', #13595, #17414, #7928, .T. ) ;
#12771=DIRECTION ( 'NONE',  ( 1.000000000000000000, 0.000000000000000000, 0.000000000000000000 ) ) ;
#12773=DIRECTION ( 'NONE',  ( 0.000000000000000000, -1.000000000000000000, 0.000000000000000000 ) ) ;
#12778=VERTEX_POINT ( 'NONE', #9746 ) ;
#12785=DIRECTION ( 'NONE',  ( 0.000000000000000000, -1.000000000000000000, 0.000000000000000000 ) ) ;
#12787=EDGE_CURVE ( 'NONE', #16231, #14736, #20800, .T. ) ;
#12803=DIRECTION ( 'NONE',  ( 0.4828336235133043330, 0.8757121056631641531, -0.000000000000000000 ) ) ;
#12810=DIRECTION ( 'NONE',  ( -0.000000000000000000, -0.000000000000000000, -1.000000000000000000 ) ) ;
#12820=DIRECTION ( 'NONE',  ( -0.000000000000000000, 0.000000000000000000, 1.000000000000000000 ) ) ;
#12824=ORIENTED_EDGE ( 'NONE', *, *, #6677, .T. ) ;
#12827=DIRECTION ( 'NONE',  ( 1.000000000000000000, 0.000000000000000000, 0.000000000000000000 ) ) ;
#12828=ORIENTED_EDGE ( 'NONE', *, *, #10676, .F. ) ;
#12832=CARTESIAN_POINT ( 'NONE',  ( 2.454813078130514813E-15, 16.67999999999999972, 14.50000000000000000 ) ) ;
#12837=AXIS2_PLACEMENT_3D ( 'NONE', #23648, #17907, #16057 ) ;
#12838=AXIS2_PLACEMENT_3D ( 'NONE', #1938, #23693, #5126 ) ;
#12839=ORIENTED_EDGE ( 'NONE', *, *, #9846, .T. ) ;
#12847=DIRECTION ( 'NONE',  ( -0.8757121056631640421, 0.4828336235133042775, 0.000000000000000000 ) ) ;
#12853=EDGE_CURVE ( 'NONE', #11189, #18498, #14175, .T. ) ;
#12858=ORIENTED_EDGE ( 'NONE', *, *, #11379, .F. ) ;
#12864=ORIENTED_EDGE ( 'NONE', *, *, #16785, .T. ) ;
#12871=CARTESIAN_POINT ( 'NONE',  ( -40.00000000000000000, -28.80990663662251450, 12.00000000000000000 ) ) ;
#12872=FACE_OUTER_BOUND ( 'NONE', #18261, .T. ) ;
#12874=ORIENTED_EDGE ( 'NONE', *, *, #1464, .F. ) ;
#12897=CARTESIAN_POINT ( 'NONE',  ( 31.10231664966676846, 45.36128193761570770, 0.000000000000000000 ) ) ;
#12905=AXIS2_PLACEMENT_3D ( 'NONE', #21998, #5399, #11095 ) ;
#12906=DIRECTION ( 'NONE',  ( 1.000000000000000000, 0.000000000000000000, -0.000000000000000000 ) ) ;
#12921=VERTEX_POINT ( 'NONE', #6495 ) ;
#12923=CARTESIAN_POINT ( 'NONE',  ( 19.85000000000000142, 16.67999999999999972, 14.50000000000000000 ) ) ;
#12930=FACE_OUTER_BOUND ( 'NONE', #1484, .T. ) ;
#12934=CARTESIAN_POINT ( 'NONE',  ( -41.00000000000000000, 4.000000000000000888, 10.49999999999999822 ) ) ;
#12936=LINE ( 'NONE', #3330, #2675 ) ;
#12940=EDGE_CURVE ( 'NONE', #4159, #9926, #19426, .T. ) ;
#12948=CARTESIAN_POINT ( 'NONE',  ( -40.00000000000000000, 29.49999999999999645, 11.00000000000000000 ) ) ;
#12950=DIRECTION ( 'NONE',  ( -0.000000000000000000, -0.000000000000000000, 1.000000000000000000 ) ) ;
#12959=CIRCLE ( 'NONE', #4002, 5.099999999999996980 ) ;
#12962=CIRCLE ( 'NONE', #4027, 1.500000000000001332 ) ;
#12969=DIRECTION ( 'NONE',  ( 1.000000000000000000, 0.000000000000000000, 0.000000000000000000 ) ) ;
#12974=CARTESIAN_POINT ( 'NONE',  ( 41.00000000000000000, 5.999999999999986677, 11.00000000000000000 ) ) ;
#12976=CYLINDRICAL_SURFACE ( 'NONE', #11813, 1.000000000000000000 ) ;
#12984=CIRCLE ( 'NONE', #4046, 1.000000000000000888 ) ;
#12996=EDGE_CURVE ( 'NONE', #10733, #11221, #3727, .T. ) ;
#12998=DIRECTION ( 'NONE',  ( -0.000000000000000000, 0.000000000000000000, 1.000000000000000000 ) ) ;
#13004=AXIS2_PLACEMENT_3D ( 'NONE', #10851, #10389, #17846 ) ;
#13005=VERTEX_POINT ( 'NONE', #10841 ) ;
#13009=CARTESIAN_POINT ( 'NONE',  ( 40.00000000000000000, -28.80990663662251450, 0.000000000000000000 ) ) ;
#13032=DIRECTION ( 'NONE',  ( -0.000000000000000000, -0.000000000000000000, 1.000000000000000000 ) ) ;
#13035=AXIS2_PLACEMENT_3D ( 'NONE', #6479, #855, #22950 ) ;
#13037=CARTESIAN_POINT ( 'NONE',  ( 29.00000000000000000, -29.50000000000000355, 11.50000000000000000 ) ) ;
#13041=ORIENTED_EDGE ( 'NONE', *, *, #10101, .F. ) ;
#13048=AXIS2_PLACEMENT_3D ( 'NONE', #22964, #8430, #2590 ) ;
#13049=VECTOR ( 'NONE', #13895, 1000.000000000000000 ) ;
#13051=EDGE_CURVE ( 'NONE', #22408, #21057, #6854, .T. ) ;
#13057=ADVANCED_FACE ( 'NONE', ( #3176 ), #3070, .T. ) ;
#13063=ORIENTED_EDGE ( 'NONE', *, *, #14281, .T. ) ;
#13065=CARTESIAN_POINT ( 'NONE',  ( -41.00000000000000000, -4.000000000000000888, 8.500000000000000000 ) ) ;
#13068=DIRECTION ( 'NONE',  ( -0.000000000000000000, -0.000000000000000000, -1.000000000000000000 ) ) ;
#13073=DIRECTION ( 'NONE',  ( -1.000000000000000000, -2.600433232233976523E-16, 0.000000000000000000 ) ) ;
#13077=CYLINDRICAL_SURFACE ( 'NONE', #3984, 1.000000000000000888 ) ;
#13079=PRODUCT ( 'End Plate', 'End Plate', '', ( #1661 ) ) ;
#13082=ORIENTED_EDGE ( 'NONE', *, *, #19031, .T. ) ;
#13085=EDGE_LOOP ( 'NONE', ( #1689, #19667 ) ) ;
#13090=CIRCLE ( 'NONE', #1036, 1.000000000000000888 ) ;
#13098=CIRCLE ( 'NONE', #6490, 21.85000000000000142 ) ;
#13103=FACE_OUTER_BOUND ( 'NONE', #465, .T. ) ;
#13114=EDGE_LOOP ( 'NONE', ( #23833, #12134, #18129, #12858 ) ) ;
#13122=DIRECTION ( 'NONE',  ( -0.8757121056631640421, -0.4828336235133042775, -0.000000000000000000 ) ) ;
#13130=CARTESIAN_POINT ( 'NONE',  ( 41.00000000000000000, -6.000000000000015099, 11.00000000000000000 ) ) ;
#13140=ORIENTED_EDGE ( 'NONE', *, *, #23354, .F. ) ;
#13151=EDGE_CURVE ( 'NONE', #12121, #12921, #10602, .T. ) ;
#13160=ADVANCED_FACE ( 'NONE', ( #5615 ), #127, .F. ) ;
#13163=DIRECTION ( 'NONE',  ( 0.000000000000000000, 0.000000000000000000, 1.000000000000000000 ) ) ;
#13164=FACE_OUTER_BOUND ( 'NONE', #24081, .T. ) ;
#13180=DIRECTION ( 'NONE',  ( -0.8757121056631641531, -0.4828336235133042775, 0.000000000000000000 ) ) ;
#13181=DIRECTION ( 'NONE',  ( 0.000000000000000000, 0.000000000000000000, 1.000000000000000000 ) ) ;
#13182=EDGE_CURVE ( 'NONE', #22169, #13221, #10717, .T. ) ;
#13186=FACE_OUTER_BOUND ( 'NONE', #22185, .T. ) ;
#13191=MECHANICAL_DESIGN_GEOMETRIC_PRESENTATION_REPRESENTATION('',(#21406),#20062);
#13197=EDGE_LOOP ( 'NONE', ( #17485, #21769, #5654, #4099 ) ) ;
#13199=CARTESIAN_POINT ( 'NONE',  ( 29.00000000000000000, -29.50000000000000355, 11.50000000000000000 ) ) ;
#13209=EDGE_LOOP ( 'NONE', ( #21797, #7666, #12135, #5568 ) ) ;
#13221=VERTEX_POINT ( 'NONE', #4155 ) ;
#13231=CARTESIAN_POINT ( 'NONE',  ( 20.64923905428956630, -37.45138642374539018, 11.00000000000000000 ) ) ;
#13266=DIRECTION ( 'NONE',  ( 1.000000000000000000, 0.000000000000000000, 0.000000000000000000 ) ) ;
#13267=FACE_OUTER_BOUND ( 'NONE', #8609, .T. ) ;
#13268=TOROIDAL_SURFACE ( 'NONE', #19530, 5.999999999999999112, 1.000000000000000000 ) ;
#13299=AXIS2_PLACEMENT_3D ( 'NONE', #18766, #249, #7529 ) ;
#13304=AXIS2_PLACEMENT_3D ( 'NONE', #9303, #23746, #14439 ) ;
#13307=EDGE_LOOP ( 'NONE', ( #14393, #14446, #14040, #13063 ) ) ;
#13321=AXIS2_PLACEMENT_3D ( 'NONE', #21859, #12695, #10615 ) ;
#13322=CIRCLE ( 'NONE', #9042, 8.000000000000003553 ) ;
#13323=EDGE_CURVE ( 'NONE', #1117, #19378, #18720, .T. ) ;
#13332=DIRECTION ( 'NONE',  ( -0.000000000000000000, 0.000000000000000000, 1.000000000000000000 ) ) ;
#13337=CARTESIAN_POINT ( 'NONE',  ( -41.00000000000000000, -5.000000000000000888, 11.00000000000000000 ) ) ;
#13339=VERTEX_POINT ( 'NONE', #7366 ) ;
#13348=EDGE_CURVE ( 'NONE', #19800, #3126, #20315, .T. ) ;
#13351=ORIENTED_EDGE ( 'NONE', *, *, #12163, .F. ) ;
#13356=DIRECTION ( 'NONE',  ( -1.000000000000000000, 2.600433232233976523E-16, -0.000000000000000000 ) ) ;
#13362=DIRECTION ( 'NONE',  ( -0.000000000000000000, -0.000000000000000000, 1.000000000000000000 ) ) ;
#13365=CARTESIAN_POINT ( 'NONE',  ( 31.10231664966676846, -45.36128193761570770, 0.000000000000000000 ) ) ;
#13377=CYLINDRICAL_SURFACE ( 'NONE', #17723, 1.000000000000000888 ) ;
#13378=DIRECTION ( 'NONE',  ( -1.000000000000000000, 0.000000000000000000, 0.000000000000000000 ) ) ;
#13379=VECTOR ( 'NONE', #2042, 1000.000000000000000 ) ;
#13381=EDGE_LOOP ( 'NONE', ( #15025, #9350, #7139, #2019 ) ) ;
#13392=DIRECTION ( 'NONE',  ( -1.000000000000000000, 0.000000000000000000, 0.000000000000000000 ) ) ;
#13406=VECTOR ( 'NONE', #4186, 1000.000000000000000 ) ;
#13412=DIRECTION ( 'NONE',  ( 1.000000000000000000, 0.000000000000000000, 0.000000000000000000 ) ) ;
#13413=CARTESIAN_POINT ( 'NONE',  ( 27.70933665152130487, -40.41277845351217479, 11.00000000000000000 ) ) ;
#13414=DIRECTION ( 'NONE',  ( -1.000000000000000000, 3.469446951953611033E-15, 0.000000000000000000 ) ) ;
#13415=AXIS2_PLACEMENT_3D ( 'NONE', #8253, #3039, #16202 ) ;
#13425=ORIENTED_EDGE ( 'NONE', *, *, #18905, .F. ) ;
#13434=DIRECTION ( 'NONE',  ( 0.000000000000000000, 1.000000000000000000, 0.000000000000000000 ) ) ;
#13446=ADVANCED_FACE ( 'NONE', ( #22883 ), #311, .F. ) ;
#13448=ORIENTED_EDGE ( 'NONE', *, *, #21367, .T. ) ;
#13454=VECTOR ( 'NONE', #18075, 1000.000000000000000 ) ;
#13459=CARTESIAN_POINT ( 'NONE',  ( 0.000000000000000000, -45.00000000000000000, 0.000000000000000000 ) ) ;
#13461=CARTESIAN_POINT ( 'NONE',  ( -47.34180362313354351, -5.000000000000002665, 10.49999999999999822 ) ) ;
#13462=EDGE_LOOP ( 'NONE', ( #6268, #16711, #7992, #9430 ) ) ;
#13463=CARTESIAN_POINT ( 'NONE',  ( 30.31394790604173295, -39.41330121100981643, 12.00000000000000000 ) ) ;
#13464=FACE_BOUND ( 'NONE', #3910, .T. ) ;
#13465=SPHERICAL_SURFACE ( 'NONE', #7881, 1.000000000000000000 ) ;
#13467=ADVANCED_FACE ( 'NONE', ( #19208 ), #18977, .F. ) ;
#13468=CIRCLE ( 'NONE', #5698, 1.000000000000000888 ) ;
#13471=CARTESIAN_POINT ( 'NONE',  ( -30.44534269664590553, 40.40463133211079594, 12.00000000000000000 ) ) ;
#13476=EDGE_CURVE ( 'NONE', #15214, #3956, #8791, .T. ) ;
#13483=CYLINDRICAL_SURFACE ( 'NONE', #20853, 5.099999999999996980 ) ;
#13493=CYLINDRICAL_SURFACE ( 'NONE', #16153, 1.000000000000002442 ) ;
#13510=AXIS2_PLACEMENT_3D ( 'NONE', #7245, #20551, #9535 ) ;
#13526=EDGE_LOOP ( 'NONE', ( #14181, #2909, #14659 ) ) ;
#13538=EDGE_LOOP ( 'NONE', ( #15630, #19818, #4748, #1476 ) ) ;
#13541=DIRECTION ( 'NONE',  ( 0.000000000000000000, -0.000000000000000000, -1.000000000000000000 ) ) ;
#13554=FACE_OUTER_BOUND ( 'NONE', #10017, .T. ) ;
#13567=CARTESIAN_POINT ( 'NONE',  ( 41.50000000000000000, -28.80990663662250739, 11.00000000000000000 ) ) ;
#13568=EDGE_CURVE ( 'NONE', #19937, #5912, #638, .T. ) ;
#13595=VERTEX_POINT ( 'NONE', #10522 ) ;
#13599=ORIENTED_EDGE ( 'NONE', *, *, #14113, .F. ) ;
#13606=DIRECTION ( 'NONE',  ( 1.000000000000000000, 0.000000000000000000, 0.000000000000000000 ) ) ;
#13641=CARTESIAN_POINT ( 'NONE',  ( -29.00000000000000000, -29.49999999999999645, 12.00000000000000000 ) ) ;
#13679=ORIENTED_EDGE ( 'NONE', *, *, #4935, .F. ) ;
#13689=ORIENTED_EDGE ( 'NONE', *, *, #8242, .T. ) ;
#13709=ORIENTED_EDGE ( 'NONE', *, *, #16785, .F. ) ;
#13715=EDGE_CURVE ( 'NONE', #20352, #9356, #19322, .T. ) ;
#13716=VERTEX_POINT ( 'NONE', #9175 ) ;
#13717=CARTESIAN_POINT ( 'NONE',  ( 29.00000000000000000, -29.50000000000000355, 12.00000000000000000 ) ) ;
#13722=EDGE_CURVE ( 'NONE', #3260, #14186, #16626, .T. ) ;
#13726=AXIS2_PLACEMENT_3D ( 'NONE', #7233, #15015, #23955 ) ;
#13729=PLANE ( 'NONE',  #23965 ) ;
#13735=CARTESIAN_POINT ( 'NONE',  ( 21.13207267780287069, 38.32709852940855910, 0.000000000000000000 ) ) ;
#13741=VECTOR ( 'NONE', #5027, 1000.000000000000000 ) ;
#13744=DIRECTION ( 'NONE',  ( -6.938893903907222856E-15, -1.000000000000000000, 0.000000000000000000 ) ) ;
#13751=EDGE_LOOP ( 'NONE', ( #4502, #3899, #3252, #9180 ) ) ;
#13762=AXIS2_PLACEMENT_3D ( 'NONE', #23750, #12624, #7134 ) ;
#13766=ORIENTED_EDGE ( 'NONE', *, *, #11291, .F. ) ;
#13768=LINE ( 'NONE', #6321, #16070 ) ;
#13771=CARTESIAN_POINT ( 'NONE',  ( -34.00000000000000000, 3.999999999999999112, 10.49999999999999822 ) ) ;
#13791=DIRECTION ( 'NONE',  ( 0.000000000000000000, 0.000000000000000000, 1.000000000000000000 ) ) ;
#13799=CARTESIAN_POINT ( 'NONE',  ( -29.00000000000000355, -3.851859888774471706E-31, 9.500000000000000000 ) ) ;
#13815=CARTESIAN_POINT ( 'NONE',  ( 0.000000000000000000, -45.00000000000000000, 0.02500000000000418554 ) ) ;
#13819=CIRCLE ( 'NONE', #21616, 5.099999999999996980 ) ;
#13822=ORIENTED_EDGE ( 'NONE', *, *, #10365, .F. ) ;
#13823=CARTESIAN_POINT ( 'NONE',  ( -41.00000000000000000, 5.000000000000000888, 9.500000000000000000 ) ) ;
#13824=TOROIDAL_SURFACE ( 'NONE', #2927, 2.000000000000000000, 1.000000000000000000 ) ;
#13833=VERTEX_POINT ( 'NONE', #7075 ) ;
#13834=CARTESIAN_POINT ( 'NONE',  ( -40.00000000000000000, -29.49999999999999645, 0.000000000000000000 ) ) ;
#13841=LINE ( 'NONE', #19931, #7155 ) ;
#13842=DIRECTION ( 'NONE',  ( 0.000000000000000000, 0.000000000000000000, -1.000000000000000000 ) ) ;
#13844=AXIS2_PLACEMENT_3D ( 'NONE', #16397, #14440, #5188 ) ;
#13852=AXIS2_PLACEMENT_3D ( 'NONE', #1714, #17954, #1593 ) ;
#13853=EDGE_CURVE ( 'NONE', #4506, #6894, #13098, .T. ) ;
#13857=VERTEX_POINT ( 'NONE', #9362 ) ;
#13871=CIRCLE ( 'NONE', #9557, 1.000000000000000888 ) ;
#13875=CARTESIAN_POINT ( 'NONE',  ( -23.90000000000000568, -29.49999999999999645, 12.00000000000000000 ) ) ;
#13895=DIRECTION ( 'NONE',  ( -0.7071067811865660024, 0.000000000000000000, -0.7071067811865291430 ) ) ;
#13901=DIRECTION ( 'NONE',  ( 1.000000000000000000, 0.000000000000000000, 0.000000000000000000 ) ) ;
#13904=PRODUCT_DEFINITION_FORMATION_WITH_SPECIFIED_SOURCE ( 'ANY', '', #13079, .NOT_KNOWN. ) ;
#13905=VECTOR ( 'NONE', #6774, 1000.000000000000000 ) ;
#13919=AXIS2_PLACEMENT_3D ( 'NONE', #23807, #1247, #1600 ) ;
#13926=EDGE_LOOP ( 'NONE', ( #22080, #10594, #10055, #13995 ) ) ;
#13932=VERTEX_POINT ( 'NONE', #3518 ) ;
#13934=LINE ( 'NONE', #14472, #14891 ) ;
#13936=ORIENTED_EDGE ( 'NONE', *, *, #5963, .T. ) ;
#13944=CARTESIAN_POINT ( 'NONE',  ( 40.00000000000000000, -28.80990663662251450, 11.00000000000000000 ) ) ;
#13948=VECTOR ( 'NONE', #3196, 1000.000000000000000 ) ;
#13957=CARTESIAN_POINT ( 'NONE',  ( 41.00000000000000000, 5.999999999999986677, 11.00000000000000000 ) ) ;
#13958=EDGE_CURVE ( 'NONE', #13716, #21260, #24022, .T. ) ;
#13964=CARTESIAN_POINT ( 'NONE',  ( -40.00000000000000000, 0.000000000000000000, 12.00000000000000000 ) ) ;
#13977=LINE ( 'NONE', #1056, #23881 ) ;
#13987=LINE ( 'NONE', #13735, #3501 ) ;
#13989=DIRECTION ( 'NONE',  ( -0.000000000000000000, -0.000000000000000000, -1.000000000000000000 ) ) ;
#13990=DIRECTION ( 'NONE',  ( 0.000000000000000000, -1.000000000000000000, 0.000000000000000000 ) ) ;
#13995=ORIENTED_EDGE ( 'NONE', *, *, #13722, .F. ) ;
#14008=EDGE_CURVE ( 'NONE', #14945, #21512, #12327, .T. ) ;
#14016=DIRECTION ( 'NONE',  ( 0.000000000000000000, -6.938893903907222067E-15, 1.000000000000000000 ) ) ;
#14017=CARTESIAN_POINT ( 'NONE',  ( 28.27483331787887977, 41.23752903419610760, 11.00000000000000000 ) ) ;
#14033=PLANE ( 'NONE',  #18953 ) ;
#14036=DIRECTION ( 'NONE',  ( -1.000000000000000000, 0.000000000000000000, 0.000000000000000000 ) ) ;
#14040=ORIENTED_EDGE ( 'NONE', *, *, #13715, .T. ) ;
#14044=FACE_OUTER_BOUND ( 'NONE', #22170, .T. ) ;
#14056=ORIENTED_EDGE ( 'NONE', *, *, #10656, .T. ) ;
#14072=DIRECTION ( 'NONE',  ( -0.5654966663575777819, -0.8247505806839220410, 0.000000000000000000 ) ) ;
#14074=VERTEX_POINT ( 'NONE', #17070 ) ;
#14077=DIRECTION ( 'NONE',  ( -1.000000000000000000, -0.000000000000000000, 0.000000000000000000 ) ) ;
#14081=EDGE_CURVE ( 'NONE', #21962, #15898, #2952, .T. ) ;
#14086=EDGE_CURVE ( 'NONE', #19209, #4885, #22823, .T. ) ;
#14092=DIRECTION ( 'NONE',  ( 0.000000000000000000, 0.000000000000000000, -1.000000000000000000 ) ) ;
#14093=CARTESIAN_POINT ( 'NONE',  ( -28.00000000000000355, -3.851859888774471706E-31, 11.00000000000000000 ) ) ;
#14109=ORIENTED_EDGE ( 'NONE', *, *, #18500, .F. ) ;
#14113=EDGE_CURVE ( 'NONE', #4922, #3497, #2801, .T. ) ;
#14120=PLANE ( 'NONE',  #16832 ) ;
#14131=ORIENTED_EDGE ( 'NONE', *, *, #7725, .F. ) ;
#14134=ORIENTED_EDGE ( 'NONE', *, *, #2269, .T. ) ;
#14145=AXIS2_PLACEMENT_3D ( 'NONE', #2312, #9725, #8142 ) ;
#14150=DIRECTION ( 'NONE',  ( -0.000000000000000000, -0.000000000000000000, -1.000000000000000000 ) ) ;
#14152=SPHERICAL_SURFACE ( 'NONE', #12500, 1.000000000000000000 ) ;
#14154=DIRECTION ( 'NONE',  ( -0.000000000000000000, 0.000000000000000000, 1.000000000000000000 ) ) ;
#14156=DIRECTION ( 'NONE',  ( 0.000000000000000000, -1.000000000000000000, 0.000000000000000000 ) ) ;
#14164=ORIENTED_EDGE ( 'NONE', *, *, #15393, .T. ) ;
#14170=LINE ( 'NONE', #21628, #16068 ) ;
#14175=CIRCLE ( 'NONE', #23548, 10.00000000000000533 ) ;
#14178=AXIS2_PLACEMENT_3D ( 'NONE', #22012, #23479, #6758 ) ;
#14181=ORIENTED_EDGE ( 'NONE', *, *, #2638, .F. ) ;
#14186=VERTEX_POINT ( 'NONE', #23190 ) ;
#14191=DIRECTION ( 'NONE',  ( -1.000000000000000000, 2.600433232233976523E-16, 0.000000000000000000 ) ) ;
#14193=VERTEX_POINT ( 'NONE', #17440 ) ;
#14194=AXIS2_PLACEMENT_3D ( 'NONE', #6167, #11387, #2143 ) ;
#14195=ORIENTED_EDGE ( 'NONE', *, *, #6248, .T. ) ;
#14196=CIRCLE ( 'NONE', #3311, 1.000000000000000222 ) ;
#14200=FACE_OUTER_BOUND ( 'NONE', #338, .T. ) ;
#14217=AXIS2_PLACEMENT_3D ( 'NONE', #2963, #18211, #9156 ) ;
#14220=FACE_OUTER_BOUND ( 'NONE', #22976, .T. ) ;
#14223=CARTESIAN_POINT ( 'NONE',  ( -42.00000000000000000, 5.000000000000002665, 8.500000000000000000 ) ) ;
#14234=AXIS2_PLACEMENT_3D ( 'NONE', #22123, #20272, #1383 ) ;
#14243=CARTESIAN_POINT ( 'NONE',  ( -41.00000000000000000, 6.000000000000000888, 12.00000000000000000 ) ) ;
#14260=VECTOR ( 'NONE', #23554, 1000.000000000000000 ) ;
#14261=VERTEX_POINT ( 'NONE', #6835 ) ;
#14267=CARTESIAN_POINT ( 'NONE',  ( -40.00000000000000000, -28.80990663662251450, 0.000000000000000000 ) ) ;
#14281=EDGE_CURVE ( 'NONE', #9356, #13857, #16436, .T. ) ;
#14290=DIRECTION ( 'NONE',  ( -0.9913301211009810654, -0.1313947906041722236, 0.000000000000000000 ) ) ;
#14293=CARTESIAN_POINT ( 'NONE',  ( 42.00000000000000711, 26.82133436441677077, 11.58578643762690241 ) ) ;
#14311=LINE ( 'NONE', #19936, #17188 ) ;
#14314=ORIENTED_EDGE ( 'NONE', *, *, #9846, .F. ) ;
#14318=DIRECTION ( 'NONE',  ( 0.000000000000000000, -1.000000000000000000, 0.000000000000000000 ) ) ;
#14319=DIRECTION ( 'NONE',  ( -0.000000000000000000, -0.000000000000000000, -1.000000000000000000 ) ) ;
#14320=DIRECTION ( 'NONE',  ( 0.000000000000000000, 0.000000000000000000, 1.000000000000000000 ) ) ;
#14324=CARTESIAN_POINT ( 'NONE',  ( 41.00000000000000000, 5.999999999999986677, 10.49999999999999822 ) ) ;
#14329=DIRECTION ( 'NONE',  ( 1.000000000000000000, 0.000000000000000000, 0.000000000000000000 ) ) ;
#14338=ORIENTED_EDGE ( 'NONE', *, *, #12476, .F. ) ;
#14354=CARTESIAN_POINT ( 'NONE',  ( -1.999999999999994449, -45.00000000000000000, 0.000000000000000000 ) ) ;
#14366=CARTESIAN_POINT ( 'NONE',  ( 33.99999999999998579, -4.000000000000013323, 9.500000000000000000 ) ) ;
#14368=EDGE_LOOP ( 'NONE', ( #18148, #8200, #6635, #5853 ) ) ;
#14377=LINE ( 'NONE', #18187, #8419 ) ;
#14378=CIRCLE ( 'NONE', #17494, 4.999999999999997335 ) ;
#14388=CARTESIAN_POINT ( 'NONE',  ( -2.983080266967717442, 45.00000000000000000, 3.000000000000002665 ) ) ;
#14393=ORIENTED_EDGE ( 'NONE', *, *, #22476, .T. ) ;
#14394=DIRECTION ( 'NONE',  ( -0.000000000000000000, 1.000000000000000000, 6.938893903907221278E-15 ) ) ;
#14411=CYLINDRICAL_SURFACE ( 'NONE', #12905, 8.000000000000003553 ) ;
#14430=ORIENTED_EDGE ( 'NONE', *, *, #622, .F. ) ;
#14431=CARTESIAN_POINT ( 'NONE',  ( 42.00000000000000000, 5.999999999999986677, 10.49999999999999822 ) ) ;
#14439=DIRECTION ( 'NONE',  ( -1.000000000000000000, 0.000000000000000000, 0.000000000000000000 ) ) ;
#14440=DIRECTION ( 'NONE',  ( 0.000000000000000000, -0.000000000000000000, -1.000000000000000000 ) ) ;
#14445=LINE ( 'NONE', #14808, #12113 ) ;
#14446=ORIENTED_EDGE ( 'NONE', *, *, #4855, .T. ) ;
#14447=EDGE_CURVE ( 'NONE', #3076, #16364, #9305, .T. ) ;
#14457=VECTOR ( 'NONE', #15443, 1000.000000000000000 ) ;
#14461=CARTESIAN_POINT ( 'NONE',  ( -29.00000000000000000, 29.49999999999999645, 11.50000000000000000 ) ) ;
#14469=AXIS2_PLACEMENT_3D ( 'NONE', #22454, #2416, #5733 ) ;
#14472=CARTESIAN_POINT ( 'NONE',  ( -42.00000000000000000, 26.82133436441678498, 11.00000000000000000 ) ) ;
#14491=AXIS2_PLACEMENT_3D ( 'NONE', #15506, #5653, #9528 ) ;
#14496=CARTESIAN_POINT ( 'NONE',  ( 30.44534269664590553, -40.40463133211081015, 11.00000000000000000 ) ) ;
#14499=DIRECTION ( 'NONE',  ( 0.000000000000000000, 0.000000000000000000, -1.000000000000000000 ) ) ;
#14511=AXIS2_PLACEMENT_3D ( 'NONE', #11444, #9621, #15216 ) ;
#14515=AXIS2_PLACEMENT_3D ( 'NONE', #18760, #9602, #21306 ) ;
#14516=ORIENTED_EDGE ( 'NONE', *, *, #17076, .F. ) ;
#14518=AXIS2_PLACEMENT_3D ( 'NONE', #14778, #16494, #20534 ) ;
#14519=LINE ( 'NONE', #16471, #18098 ) ;
#14522=CARTESIAN_POINT ( 'NONE',  ( 0.000000000000000000, -45.00000000000000000, 0.000000000000000000 ) ) ;
#14523=CIRCLE ( 'NONE', #19620, 49.00000000000000000 ) ;
#14538=AXIS2_PLACEMENT_3D ( 'NONE', #18692, #14669, #12827 ) ;
#14539=ORIENTED_EDGE ( 'NONE', *, *, #155, .F. ) ;
#14550=AXIS2_PLACEMENT_3D ( 'NONE', #1709, #7190, #5734 ) ;
#14551=EDGE_LOOP ( 'NONE', ( #3095, #8767, #20251, #9339 ) ) ;
#14556=DIRECTION ( 'NONE',  ( 1.000000000000000000, 0.000000000000000000, -0.000000000000000000 ) ) ;
#14558=CYLINDRICAL_SURFACE ( 'NONE', #17251, 1.000000000000000888 ) ;
#14564=DIRECTION ( 'NONE',  ( 1.000000000000000000, 0.000000000000000000, 0.000000000000000000 ) ) ;
#14565=EDGE_CURVE ( 'NONE', #14193, #14261, #21272, .T. ) ;
#14572=CARTESIAN_POINT ( 'NONE',  ( 30.44534269664590553, 40.40463133211080304, 12.00000000000000000 ) ) ;
#14590=LINE ( 'NONE', #5338, #13948 ) ;
#14610=ORIENTED_EDGE ( 'NONE', *, *, #12426, .T. ) ;
#14628=EDGE_CURVE ( 'NONE', #3956, #16460, #13871, .T. ) ;
#14631=ADVANCED_FACE ( 'NONE', ( #933 ), #8588, .F. ) ;
#14639=CARTESIAN_POINT ( 'NONE',  ( 33.99999999999998579, -5.000000000000013323, 11.00000000000000000 ) ) ;
#14641=CIRCLE ( 'NONE', #17773, 1.999999999999994449 ) ;
#14645=CARTESIAN_POINT ( 'NONE',  ( 30.31394790604173295, 39.41330121100981643, 12.00000000000000000 ) ) ;
#14651=CYLINDRICAL_SURFACE ( 'NONE', #14234, 8.000000000000003553 ) ;
#14659=ORIENTED_EDGE ( 'NONE', *, *, #5440, .F. ) ;
#14669=DIRECTION ( 'NONE',  ( -0.000000000000000000, 0.000000000000000000, 1.000000000000000000 ) ) ;
#14688=DIRECTION ( 'NONE',  ( -0.000000000000000000, -0.000000000000000000, -1.000000000000000000 ) ) ;
#14690=ORIENTED_EDGE ( 'NONE', *, *, #21397, .T. ) ;
#14697=DIRECTION ( 'NONE',  ( 0.000000000000000000, -1.000000000000000000, 0.000000000000000000 ) ) ;
#14699=DIRECTION ( 'NONE',  ( 0.000000000000000000, -1.000000000000000000, 0.000000000000000000 ) ) ;
#14700=DIRECTION ( 'NONE',  ( 1.000000000000000000, 0.000000000000000000, 0.000000000000000000 ) ) ;
#14701=DIRECTION ( 'NONE',  ( 1.000000000000000000, 2.775557561562888984E-15, 0.000000000000000000 ) ) ;
#14707=EDGE_CURVE ( 'NONE', #19489, #5826, #14641, .T. ) ;
#14708=FACE_OUTER_BOUND ( 'NONE', #21439, .T. ) ;
#14713=CARTESIAN_POINT ( 'NONE',  ( -42.00000000000000000, -26.82133436441678853, 12.00000000000000000 ) ) ;
#14719=CARTESIAN_POINT ( 'NONE',  ( 41.00000000000000000, 3.999999999999987121, 10.49999999999999822 ) ) ;
#14724=FACE_OUTER_BOUND ( 'NONE', #5494, .T. ) ;
#14729=DIRECTION ( 'NONE',  ( 0.8571673007021116675, 1.049727191138617833E-16, -0.5150380749100552658 ) ) ;
#14731=ORIENTED_EDGE ( 'NONE', *, *, #3459, .F. ) ;
#14736=VERTEX_POINT ( 'NONE', #5535 ) ;
#14737=VECTOR ( 'NONE', #23599, 1000.000000000000000 ) ;
#14743=CARTESIAN_POINT ( 'NONE',  ( 41.00000000000000000, -4.000000000000015099, 10.49999999999999822 ) ) ;
#14760=EDGE_CURVE ( 'NONE', #9485, #758, #12288, .T. ) ;
#14765=ADVANCED_FACE ( 'NONE', ( #5181 ), #8946, .T. ) ;
#14773=CARTESIAN_POINT ( 'NONE',  ( 34.10000000000000142, -29.50000000000000355, 11.50000000000000000 ) ) ;
#14775=FACE_OUTER_BOUND ( 'NONE', #11712, .T. ) ;
#14776=AXIS2_PLACEMENT_3D ( 'NONE', #5184, #22035, #12491 ) ;
#14778=CARTESIAN_POINT ( 'NONE',  ( 30.31394790604173295, 39.41330121100981643, 11.00000000000000000 ) ) ;
#14786=ADVANCED_FACE ( 'NONE', ( #15974 ), #16219, .F. ) ;
#14796=DIRECTION ( 'NONE',  ( -1.000000000000000000, 0.000000000000000000, 0.000000000000000000 ) ) ;
#14800=DIRECTION ( 'NONE',  ( 0.000000000000000000, -1.000000000000000000, 0.000000000000000000 ) ) ;
#14808=CARTESIAN_POINT ( 'NONE',  ( 2.024999999999999911, -45.00000000000000000, 0.000000000000000000 ) ) ;
#14824=CARTESIAN_POINT ( 'NONE',  ( -34.10000000000000142, -29.49999999999999645, 11.50000000000000000 ) ) ;
#14829=CARTESIAN_POINT ( 'NONE',  ( 1.041919733032276918, 45.00000000000000000, 0.000000000000000000 ) ) ;
#14831=EDGE_CURVE ( 'NONE', #18239, #3246, #19522, .T. ) ;
#14832=DIRECTION ( 'NONE',  ( 0.000000000000000000, 0.000000000000000000, -1.000000000000000000 ) ) ;
#14841=AXIS2_PLACEMENT_3D ( 'NONE', #12649, #220, #7498 ) ;
#14866=DIRECTION ( 'NONE',  ( -1.000000000000000000, 0.000000000000000000, 0.000000000000000000 ) ) ;
#14870=FACE_OUTER_BOUND ( 'NONE', #20442, .T. ) ;
#14882=DIRECTION ( 'NONE',  ( 1.000000000000000000, 0.000000000000000000, 0.000000000000000000 ) ) ;
#14891=VECTOR ( 'NONE', #18282, 1000.000000000000000 ) ;
#14900=CARTESIAN_POINT ( 'NONE',  ( -34.00000000000000000, 4.999999999999999112, 9.500000000000000000 ) ) ;
#14908=CYLINDRICAL_SURFACE ( 'NONE', #23124, 1.000000000000000888 ) ;
#14909=VERTEX_POINT ( 'NONE', #14963 ) ;
#14913=ORIENTED_EDGE ( 'NONE', *, *, #17891, .F. ) ;
#14919=TOROIDAL_SURFACE ( 'NONE', #3257, 2.000000000000000000, 1.000000000000000000 ) ;
#14921=CARTESIAN_POINT ( 'NONE',  ( 42.00000000000000000, -4.000000000000015099, 10.49999999999999822 ) ) ;
#14924=VECTOR ( 'NONE', #17237, 1000.000000000000000 ) ;
#14928=CIRCLE ( 'NONE', #12206, 4.000000000000000000 ) ;
#14945=VERTEX_POINT ( 'NONE', #21202 ) ;
#14960=ORIENTED_EDGE ( 'NONE', *, *, #10492, .T. ) ;
#14962=CIRCLE ( 'NONE', #6028, 1.000000000000000444 ) ;
#14963=CARTESIAN_POINT ( 'NONE',  ( -40.00000000000000000, 29.49999999999999645, 11.00000000000000000 ) ) ;
#14971=ADVANCED_FACE ( 'NONE', ( #2404 ), #22662, .F. ) ;
#14978=CARTESIAN_POINT ( 'NONE',  ( -41.00000000000000000, 26.23076770084981391, 12.00000000000000000 ) ) ;
#14981=DIRECTION ( 'NONE',  ( -1.000000000000000000, 0.000000000000000000, 0.000000000000000000 ) ) ;
#14996=LINE ( 'NONE', #9731, #15811 ) ;
#15001=DIRECTION ( 'NONE',  ( 1.000000000000000000, 2.600433232233976523E-16, 0.000000000000000000 ) ) ;
#15015=DIRECTION ( 'NONE',  ( 0.000000000000000000, -0.000000000000000000, -1.000000000000000000 ) ) ;
#15025=ORIENTED_EDGE ( 'NONE', *, *, #12498, .T. ) ;
#15029=CARTESIAN_POINT ( 'NONE',  ( -40.00000000000000000, -29.49999999999999645, 12.00000000000000000 ) ) ;
#15032=ORIENTED_EDGE ( 'NONE', *, *, #19154, .T. ) ;
#15036=EDGE_LOOP ( 'NONE', ( #15161, #1926 ) ) ;
#15041=VECTOR ( 'NONE', #12785, 1000.000000000000000 ) ;
#15046=CARTESIAN_POINT ( 'NONE',  ( 40.00000000000000000, 28.80990663662251450, 11.00000000000000000 ) ) ;
#15050=ORIENTED_EDGE ( 'NONE', *, *, #22303, .T. ) ;
#15051=EDGE_CURVE ( 'NONE', #22790, #3124, #202, .T. ) ;
#15057=EDGE_CURVE ( 'NONE', #1666, #7729, #2773, .T. ) ;
#15064=ADVANCED_FACE ( 'NONE', ( #19496 ), #6923, .F. ) ;
#15068=EDGE_LOOP ( 'NONE', ( #20475, #14056, #7263, #23801 ) ) ;
#15073=CARTESIAN_POINT ( 'NONE',  ( 41.00000000000000000, -4.000000000000015099, 10.49999999999999822 ) ) ;
#15095=CARTESIAN_POINT ( 'NONE',  ( -41.00000000000000000, -26.23076770084981746, 12.00000000000000000 ) ) ;
#15102=ORIENTED_EDGE ( 'NONE', *, *, #963, .T. ) ;
#15104=EDGE_LOOP ( 'NONE', ( #14690, #18232, #2582, #10465 ) ) ;
#15110=EDGE_CURVE ( 'NONE', #2102, #7962, #16159, .T. ) ;
#15111=FACE_OUTER_BOUND ( 'NONE', #10090, .T. ) ;
#15114=VERTEX_POINT ( 'NONE', #17528 ) ;
#15129=CARTESIAN_POINT ( 'NONE',  ( 41.00000000000000000, 3.999999999999987121, 9.500000000000000000 ) ) ;
#15138=ORIENTED_EDGE ( 'NONE', *, *, #11948, .T. ) ;
#15140=DIRECTION ( 'NONE',  ( 0.000000000000000000, 0.000000000000000000, 1.000000000000000000 ) ) ;
#15144=ORIENTED_EDGE ( 'NONE', *, *, #9808, .T. ) ;
#15147=FACE_OUTER_BOUND ( 'NONE', #8266, .T. ) ;
#15148=CARTESIAN_POINT ( 'NONE',  ( 41.50000000000000000, 28.80990663662250739, 11.00000000000000000 ) ) ;
#15153=CARTESIAN_POINT ( 'NONE',  ( 41.50000000000000000, 28.80990663662250739, 12.00000000000000000 ) ) ;
#15160=CARTESIAN_POINT ( 'NONE',  ( -20.84999999999999787, -16.67999999999985050, 13.00000000000000178 ) ) ;
#15161=ORIENTED_EDGE ( 'NONE', *, *, #12787, .T. ) ;
#15169=CARTESIAN_POINT ( 'NONE',  ( -42.00000000000000000, 6.000000000000001776, 11.00000000000000000 ) ) ;
#15171=CARTESIAN_POINT ( 'NONE',  ( 39.00000000000000000, -28.80990663662251805, 12.00000000000000000 ) ) ;
#15177=CARTESIAN_POINT ( 'NONE',  ( 39.00000000000000000, 28.80990663662251805, 12.00000000000000000 ) ) ;
#15181=DIRECTION ( 'NONE',  ( 1.000000000000000000, 3.469446951953611033E-15, 0.000000000000000000 ) ) ;
#15187=ORIENTED_EDGE ( 'NONE', *, *, #3440, .F. ) ;
#15194=UNCERTAINTY_MEASURE_WITH_UNIT (LENGTH_MEASURE( 1.000000000000000082E-05 ), #10487, 'distance_accuracy_value', 'NONE');
#15197=CARTESIAN_POINT ( 'NONE',  ( -41.00000000000000000, -6.000000000000000888, 12.00000000000000000 ) ) ;
#15198=DIRECTION ( 'NONE',  ( 0.000000000000000000, -0.000000000000000000, -1.000000000000000000 ) ) ;
#15214=VERTEX_POINT ( 'NONE', #10680 ) ;
#15216=DIRECTION ( 'NONE',  ( 1.000000000000000000, 0.000000000000000000, 0.000000000000000000 ) ) ;
#15230=DIRECTION ( 'NONE',  ( 1.000000000000000000, 0.000000000000000000, 0.000000000000000000 ) ) ;
#15231=DIRECTION ( 'NONE',  ( -0.000000000000000000, 1.000000000000000000, -0.000000000000000000 ) ) ;
#15234=EDGE_CURVE ( 'NONE', #15114, #12189, #8758, .T. ) ;
#15239=LINE ( 'NONE', #20897, #13406 ) ;
#15245=CIRCLE ( 'NONE', #10592, 4.999999999999997335 ) ;
#15249=ORIENTED_EDGE ( 'NONE', *, *, #19924, .T. ) ;
#15254=ORIENTED_EDGE ( 'NONE', *, *, #1123, .F. ) ;
#15256=EDGE_LOOP ( 'NONE', ( #3071, #3193 ) ) ;
#15258=VECTOR ( 'NONE', #23420, 1000.000000000000000 ) ;
#15265=ORIENTED_EDGE ( 'NONE', *, *, #12426, .F. ) ;
#15267=DIRECTION ( 'NONE',  ( 0.000000000000000000, 0.000000000000000000, 1.000000000000000000 ) ) ;
#15270=FACE_OUTER_BOUND ( 'NONE', #15068, .T. ) ;
#15289=CIRCLE ( 'NONE', #2440, 1.500000000000001332 ) ;
#15300=DIRECTION ( 'NONE',  ( 1.000000000000000000, -6.938893903907232322E-15, 0.000000000000000000 ) ) ;
#15309=DIRECTION ( 'NONE',  ( 1.000000000000000000, 0.000000000000000000, 0.000000000000000000 ) ) ;
#15310=CIRCLE ( 'NONE', #21583, 4.999999999999997335 ) ;
#15325=VECTOR ( 'NONE', #17482, 1000.000000000000000 ) ;
#15328=CARTESIAN_POINT ( 'NONE',  ( -47.34180362313354351, -6.000000000000002665, 11.00000000000000000 ) ) ;
#15331=EDGE_CURVE ( 'NONE', #8760, #24045, #15289, .T. ) ;
#15346=AXIS2_PLACEMENT_3D ( 'NONE', #18567, #13163, #1845 ) ;
#15347=VERTEX_POINT ( 'NONE', #11380 ) ;
#15353=CARTESIAN_POINT ( 'NONE',  ( 0.000000000000000000, -45.00000000000000000, 3.000000000000002665 ) ) ;
#15354=VECTOR ( 'NONE', #13362, 1000.000000000000000 ) ;
#15366=CIRCLE ( 'NONE', #23182, 1.000000000000000888 ) ;
#15367=CARTESIAN_POINT ( 'NONE',  ( 1.999999999999994449, -45.00000000000000000, 3.000000000000002665 ) ) ;
#15376=LINE ( 'NONE', #21005, #2049 ) ;
#15377=CARTESIAN_POINT ( 'NONE',  ( -40.00000000000000000, 0.000000000000000000, 0.000000000000000000 ) ) ;
#15385=CARTESIAN_POINT ( 'NONE',  ( -29.00000000000000000, -29.49999999999999645, 12.00000000000000000 ) ) ;
#15389=ORIENTED_EDGE ( 'NONE', *, *, #16207, .T. ) ;
#15393=EDGE_CURVE ( 'NONE', #15853, #11189, #8282, .T. ) ;
#15399=LINE ( 'NONE', #11718, #1624 ) ;
#15405=CARTESIAN_POINT ( 'NONE',  ( -30.31394790604173650, 39.41330121100982353, 12.00000000000000000 ) ) ;
#15407=LINE ( 'NONE', #17368, #2453 ) ;
#15409=LINE ( 'NONE', #11981, #7571 ) ;
#15411=DIRECTION ( 'NONE',  ( 0.000000000000000000, 0.000000000000000000, 1.000000000000000000 ) ) ;
#15430=CIRCLE ( 'NONE', #652, 19.84999999999999787 ) ;
#15443=DIRECTION ( 'NONE',  ( -0.000000000000000000, -0.000000000000000000, -1.000000000000000000 ) ) ;
#15444=DIRECTION ( 'NONE',  ( -1.000000000000000000, 0.000000000000000000, 0.000000000000000000 ) ) ;
#15449=EDGE_CURVE ( 'NONE', #3126, #4922, #22031, .T. ) ;
#15450=ORIENTED_EDGE ( 'NONE', *, *, #4768, .T. ) ;
#15451=ORIENTED_EDGE ( 'NONE', *, *, #630, .F. ) ;
#15456=EDGE_CURVE ( 'NONE', #3740, #12921, #6753, .T. ) ;
#15479=CARTESIAN_POINT ( 'NONE',  ( -34.00000000000000000, -4.999999999999999112, 10.49999999999999822 ) ) ;
#15488=CARTESIAN_POINT ( 'NONE',  ( 40.00000000000000000, 0.000000000000000000, 12.00000000000000000 ) ) ;
#15489=VERTEX_POINT ( 'NONE', #8804 ) ;
#15492=DIRECTION ( 'NONE',  ( 0.000000000000000000, 0.000000000000000000, 1.000000000000000000 ) ) ;
#15494=ADVANCED_FACE ( 'NONE', ( #5144 ), #9029, .T. ) ;
#15506=CARTESIAN_POINT ( 'NONE',  ( 0.000000000000000000, 0.000000000000000000, 0.000000000000000000 ) ) ;
#15508=VERTEX_POINT ( 'NONE', #10743 ) ;
#15517=EDGE_LOOP ( 'NONE', ( #22030, #10921, #292, #20982 ) ) ;
#15520=DIRECTION ( 'NONE',  ( -0.8247505806839219300, 0.5654966663575777819, -2.861428388275804004E-15 ) ) ;
#15572=DIRECTION ( 'NONE',  ( 0.000000000000000000, -0.000000000000000000, -1.000000000000000000 ) ) ;
#15574=CARTESIAN_POINT ( 'NONE',  ( 41.00000000000000000, -5.000000000000015099, 11.00000000000000000 ) ) ;
#15579=CARTESIAN_POINT ( 'NONE',  ( 19.85000000000000142, -16.67999999999999616, 13.50000000000000178 ) ) ;
#15589=DIRECTION ( 'NONE',  ( 1.000000000000000000, 0.000000000000000000, 0.000000000000000000 ) ) ;
#15594=LINE ( 'NONE', #6709, #10727 ) ;
#15599=ORIENTED_EDGE ( 'NONE', *, *, #16508, .F. ) ;
#15600=CIRCLE ( 'NONE', #40, 8.000000000000003553 ) ;
#15604=DIRECTION ( 'NONE',  ( 1.000000000000000000, 0.000000000000000000, 0.000000000000000000 ) ) ;
#15605=DIRECTION ( 'NONE',  ( 0.000000000000000000, -1.000000000000000000, 0.000000000000000000 ) ) ;
#15607=EDGE_CURVE ( 'NONE', #11723, #10733, #14523, .T. ) ;
#15619=EDGE_LOOP ( 'NONE', ( #9774, #12729 ) ) ;
#15630=ORIENTED_EDGE ( 'NONE', *, *, #16877, .F. ) ;
#15633=ADVANCED_FACE ( 'NONE', ( #12930 ), #4839, .T. ) ;
#15642=ORIENTED_EDGE ( 'NONE', *, *, #2218, .T. ) ;
#15646=ORIENTED_EDGE ( 'NONE', *, *, #17847, .F. ) ;
#15655=ORIENTED_EDGE ( 'NONE', *, *, #21395, .F. ) ;
#15670=ORIENTED_EDGE ( 'NONE', *, *, #19608, .T. ) ;
#15674=CARTESIAN_POINT ( 'NONE',  ( -0.9830802669677229932, 45.00000000000000000, 0.000000000000000000 ) ) ;
#15683=CYLINDRICAL_SURFACE ( 'NONE', #5879, 4.999999999999997335 ) ;
#15693=APPLICATION_CONTEXT ( 'automotive_design' ) ;
#15698=CARTESIAN_POINT ( 'NONE',  ( -42.00000000000000711, 26.82133436441678498, 0.000000000000000000 ) ) ;
#15700=CARTESIAN_POINT ( 'NONE',  ( 2.454813078130514813E-15, -16.67999999999999972, 12.00000000000000000 ) ) ;
#15710=DIRECTION ( 'NONE',  ( 1.000000000000000000, 0.000000000000000000, 0.000000000000000000 ) ) ;
#15713=CARTESIAN_POINT ( 'NONE',  ( -41.00000000000000000, 5.000000000000000888, 10.49999999999999822 ) ) ;
#15724=EDGE_CURVE ( 'NONE', #555, #15898, #2465, .T. ) ;
#15750=AXIS2_PLACEMENT_3D ( 'NONE', #23385, #14320, #23626 ) ;
#15755=AXIS2_PLACEMENT_3D ( 'NONE', #6941, #10698, #8979 ) ;
#15768=DIRECTION ( 'NONE',  ( 0.000000000000000000, 1.000000000000000000, 0.000000000000000000 ) ) ;
#15769=EDGE_CURVE ( 'NONE', #20616, #9207, #17670, .T. ) ;
#15780=FACE_BOUND ( 'NONE', #22154, .T. ) ;
#15791=EDGE_CURVE ( 'NONE', #16259, #8265, #2074, .T. ) ;
#15797=ORIENTED_EDGE ( 'NONE', *, *, #20746, .F. ) ;
#15803=ORIENTED_EDGE ( 'NONE', *, *, #21834, .T. ) ;
#15806=CARTESIAN_POINT ( 'NONE',  ( 39.00000000000000000, 0.000000000000000000, 11.00000000000000000 ) ) ;
#15810=CARTESIAN_POINT ( 'NONE',  ( 29.00000000000000000, 29.50000000000000355, 11.50000000000000000 ) ) ;
#15811=VECTOR ( 'NONE', #11200, 1000.000000000000000 ) ;
#15815=VECTOR ( 'NONE', #16399, 1000.000000000000000 ) ;
#15840=VERTEX_POINT ( 'NONE', #7301 ) ;
#15843=ORIENTED_EDGE ( 'NONE', *, *, #20282, .F. ) ;
#15850=CARTESIAN_POINT ( 'NONE',  ( 19.85000000000000142, 16.67999999999999972, 14.50000000000000000 ) ) ;
#15853=VERTEX_POINT ( 'NONE', #20604 ) ;
#15871=DIRECTION ( 'NONE',  ( 0.000000000000000000, -1.000000000000000000, 0.000000000000000000 ) ) ;
#15875=FACE_OUTER_BOUND ( 'NONE', #13381, .T. ) ;
#15879=ORIENTED_EDGE ( 'NONE', *, *, #21860, .F. ) ;
#15887=DIRECTION ( 'NONE',  ( -0.000000000000000000, -0.000000000000000000, -1.000000000000000000 ) ) ;
#15894=DIRECTION ( 'NONE',  ( 1.000000000000000000, 0.000000000000000000, 0.000000000000000000 ) ) ;
#15898=VERTEX_POINT ( 'NONE', #20486 ) ;
#15906=FACE_OUTER_BOUND ( 'NONE', #23016, .T. ) ;
#15911=EDGE_CURVE ( 'NONE', #23101, #19750, #18757, .T. ) ;
#15921=LINE ( 'NONE', #8580, #21603 ) ;
#15925=CARTESIAN_POINT ( 'NONE',  ( 42.00000000000000000, -4.000000000000015099, 8.500000000000000000 ) ) ;
#15937=EDGE_CURVE ( 'NONE', #2256, #17414, #3882, .T. ) ;
#15954=ADVANCED_FACE ( 'NONE', ( #11177 ), #18654, .T. ) ;
#15956=DIRECTION ( 'NONE',  ( 0.000000000000000000, 1.000000000000000000, 0.000000000000000000 ) ) ;
#15966=EDGE_LOOP ( 'NONE', ( #23380, #21253, #22884, #8496 ) ) ;
#15972=CIRCLE ( 'NONE', #22999, 1.000000000000000000 ) ;
#15974=FACE_OUTER_BOUND ( 'NONE', #9777, .T. ) ;
#15979=DIRECTION ( 'NONE',  ( -1.000000000000000000, 0.000000000000000000, 0.000000000000000000 ) ) ;
#15987=CARTESIAN_POINT ( 'NONE',  ( 30.44534269664590553, -40.40463133211081015, 12.00000000000000000 ) ) ;
#15995=LINE ( 'NONE', #16352, #23571 ) ;
#16010=EDGE_LOOP ( 'NONE', ( #21506, #16406, #7882, #16156 ) ) ;
#16012=CARTESIAN_POINT ( 'NONE',  ( -29.00000000000000000, 29.49999999999999645, 11.50000000000000000 ) ) ;
#16024=ORIENTED_EDGE ( 'NONE', *, *, #21560, .T. ) ;
#16037=EDGE_LOOP ( 'NONE', ( #1844, #5216, #18632, #12864 ) ) ;
#16039=CARTESIAN_POINT ( 'NONE',  ( 21.85000000000000497, 0.000000000000000000, 12.00000000000000000 ) ) ;
#16049=CIRCLE ( 'NONE', #5139, 1.000000000000000888 ) ;
#16050=AXIS2_PLACEMENT_3D ( 'NONE', #6667, #10665, #16286 ) ;
#16057=DIRECTION ( 'NONE',  ( 1.000000000000000000, 0.000000000000000000, 0.000000000000000000 ) ) ;
#16058=EDGE_LOOP ( 'NONE', ( #5906, #22231, #16773, #5505 ) ) ;
#16063=CARTESIAN_POINT ( 'NONE',  ( -34.00000000000000000, 4.999999999999999112, 11.00000000000000000 ) ) ;
#16068=VECTOR ( 'NONE', #8551, 1000.000000000000000 ) ;
#16070=VECTOR ( 'NONE', #21217, 1000.000000000000000 ) ;
#16071=DIRECTION ( 'NONE',  ( 1.000000000000000000, 0.000000000000000000, 0.000000000000000000 ) ) ;
#16073=CIRCLE ( 'NONE', #19986, 11.00000000000000711 ) ;
#16081=EDGE_LOOP ( 'NONE', ( #17952, #18454, #16973, #9533 ) ) ;
#16086=FACE_OUTER_BOUND ( 'NONE', #15104, .T. ) ;
#16092=CARTESIAN_POINT ( 'NONE',  ( -34.00000000000000000, 5.999999999999999112, 11.00000000000000000 ) ) ;
#16095=VERTEX_POINT ( 'NONE', #12285 ) ;
#16097=DIRECTION ( 'NONE',  ( -1.000000000000000000, 0.000000000000000000, 0.000000000000000000 ) ) ;
#16098=DIRECTION ( 'NONE',  ( -1.000000000000000000, 0.000000000000000000, 0.000000000000000000 ) ) ;
#16100=CARTESIAN_POINT ( 'NONE',  ( 0.000000000000000000, -45.00000000000000000, 0.000000000000000000 ) ) ;
#16102=( BOUNDED_CURVE ( )  B_SPLINE_CURVE ( 3, ( #16779, #2155, #9585, #7285 ),
 .UNSPECIFIED., .F., .T. ) 
 B_SPLINE_CURVE_WITH_KNOTS ( ( 4, 4 ),
 ( 4.712388980384689674, 6.283185307179586232 ),
 .UNSPECIFIED. ) 
 CURVE ( )  GEOMETRIC_REPRESENTATION_ITEM ( )  RATIONAL_B_SPLINE_CURVE ( ( 1.000000000000000000, 0.8047378541243649375, 0.8047378541243649375, 1.000000000000000000 ) ) 
 REPRESENTATION_ITEM ( '' )  );
#16110=DIRECTION ( 'NONE',  ( 0.000000000000000000, 0.000000000000000000, -1.000000000000000000 ) ) ;
#16113=AXIS2_PLACEMENT_3D ( 'NONE', #15153, #17117, #14701 ) ;
#16118=VECTOR ( 'NONE', #11617, 1000.000000000000000 ) ;
#16136=AXIS2_PLACEMENT_3D ( 'NONE', #22881, #15411, #10027 ) ;
#16137=AXIS2_PLACEMENT_3D ( 'NONE', #10997, #16641, #7358 ) ;
#16150=AXIS2_PLACEMENT_3D ( 'NONE', #3429, #21493, #8546 ) ;
#16153=AXIS2_PLACEMENT_3D ( 'NONE', #13231, #2379, #7617 ) ;
#16156=ORIENTED_EDGE ( 'NONE', *, *, #7725, .T. ) ;
#16159=CIRCLE ( 'NONE', #4899, 1.000000000000000888 ) ;
#16160=DIRECTION ( 'NONE',  ( -1.000000000000000000, 0.000000000000000000, 0.000000000000000000 ) ) ;
#16161=CARTESIAN_POINT ( 'NONE',  ( 41.50000000000000000, 28.80990663662250739, 12.00000000000000000 ) ) ;
#16166=DIRECTION ( 'NONE',  ( -1.000000000000000000, 0.000000000000000000, 0.000000000000000000 ) ) ;
#16172=DIRECTION ( 'NONE',  ( -0.000000000000000000, 0.000000000000000000, 1.000000000000000000 ) ) ;
#16178=CARTESIAN_POINT ( 'NONE',  ( 29.00000000000000000, -29.50000000000000355, 0.000000000000000000 ) ) ;
#16182=ORIENTED_EDGE ( 'NONE', *, *, #13958, .F. ) ;
#16202=DIRECTION ( 'NONE',  ( -1.000000000000000000, 0.000000000000000000, 0.000000000000000000 ) ) ;
#16205=DIRECTION ( 'NONE',  ( -0.000000000000000000, 0.000000000000000000, 1.000000000000000000 ) ) ;
#16207=EDGE_CURVE ( 'NONE', #10216, #19750, #23996, .T. ) ;
#16210=DIRECTION ( 'NONE',  ( 1.000000000000000000, 0.000000000000000000, -0.000000000000000000 ) ) ;
#16219=CONICAL_SURFACE ( 'NONE', #11913, 2.024999999999999911, 0.7853981633974743692 ) ;
#16231=VERTEX_POINT ( 'NONE', #18734 ) ;
#16242=TOROIDAL_SURFACE ( 'NONE', #3371, 2.000000000000000000, 1.000000000000000000 ) ;
#16249=DIRECTION ( 'NONE',  ( -1.000000000000000000, 0.000000000000000000, 0.000000000000000000 ) ) ;
#16253=ORIENTED_EDGE ( 'NONE', *, *, #13853, .T. ) ;
#16255=LINE ( 'NONE', #2546, #2539 ) ;
#16259=VERTEX_POINT ( 'NONE', #18506 ) ;
#16270=ORIENTED_EDGE ( 'NONE', *, *, #5164, .F. ) ;
#16286=DIRECTION ( 'NONE',  ( -1.000000000000000000, 0.000000000000000000, 0.000000000000000000 ) ) ;
#16288=VECTOR ( 'NONE', #17478, 1000.000000000000000 ) ;
#16302=DIRECTION ( 'NONE',  ( -0.9913301211009810654, 0.1313947906041722236, -3.439367267033602767E-15 ) ) ;
#16304=DIRECTION ( 'NONE',  ( -0.000000000000000000, 0.000000000000000000, 1.000000000000000000 ) ) ;
#16331=CARTESIAN_POINT ( 'NONE',  ( -0.9830802669677229932, 45.00000000000000000, 0.000000000000000000 ) ) ;
#16333=VECTOR ( 'NONE', #17506, 1000.000000000000000 ) ;
#16352=CARTESIAN_POINT ( 'NONE',  ( 40.77574956473004164, 27.49633847812775755, 12.00000000000000000 ) ) ;
#16355=EDGE_CURVE ( 'NONE', #14736, #16231, #21192, .T. ) ;
#16364=VERTEX_POINT ( 'NONE', #5920 ) ;
#16367=EDGE_LOOP ( 'NONE', ( #4412, #18840, #17492, #10674 ) ) ;
#16368=DIRECTION ( 'NONE',  ( 0.000000000000000000, 0.000000000000000000, 1.000000000000000000 ) ) ;
#16372=CARTESIAN_POINT ( 'NONE',  ( 47.34180362313352930, -6.000000000000016875, 11.00000000000000000 ) ) ;
#16374=TOROIDAL_SURFACE ( 'NONE', #19515, 5.999999999999999112, 1.000000000000000000 ) ;
#16379=VERTEX_POINT ( 'NONE', #324 ) ;
#16389=CARTESIAN_POINT ( 'NONE',  ( -20.64923905428956630, 37.45138642374539018, 11.00000000000000000 ) ) ;
#16392=VECTOR ( 'NONE', #6559, 1000.000000000000000 ) ;
#16397=CARTESIAN_POINT ( 'NONE',  ( -29.00000000000000000, -29.49999999999999645, 11.00000000000000000 ) ) ;
#16399=DIRECTION ( 'NONE',  ( -0.000000000000000000, -0.000000000000000000, -1.000000000000000000 ) ) ;
#16406=ORIENTED_EDGE ( 'NONE', *, *, #1639, .F. ) ;
#16407=EDGE_LOOP ( 'NONE', ( #17591, #1499, #12754, #16766 ) ) ;
#16408=ADVANCED_FACE ( 'NONE', ( #20821 ), #13493, .T. ) ;
#16414=DIRECTION ( 'NONE',  ( -0.000000000000000000, 1.000000000000000000, -0.000000000000000000 ) ) ;
#16424=ORIENTED_EDGE ( 'NONE', *, *, #22174, .T. ) ;
#16425=DIRECTION ( 'NONE',  ( 0.000000000000000000, 0.000000000000000000, -1.000000000000000000 ) ) ;
#16434=ORIENTED_EDGE ( 'NONE', *, *, #8706, .F. ) ;
#16436=LINE ( 'NONE', #23903, #15041 ) ;
#16439=EDGE_CURVE ( 'NONE', #16829, #20146, #16894, .T. ) ;
#16446=CIRCLE ( 'NONE', #19591, 50.00000000000000000 ) ;
#16460=VERTEX_POINT ( 'NONE', #20686 ) ;
#16465=VECTOR ( 'NONE', #17327, 1000.000000000000000 ) ;
#16471=CARTESIAN_POINT ( 'NONE',  ( 20.85000000000000497, -16.67999999999999616, 14.50000000000000000 ) ) ;
#16474=ADVANCED_FACE ( 'NONE', ( #22897 ), #3969, .F. ) ;
#16480=DIRECTION ( 'NONE',  ( 1.000000000000000000, 0.000000000000000000, 0.000000000000000000 ) ) ;
#16484=ORIENTED_EDGE ( 'NONE', *, *, #7448, .T. ) ;
#16494=DIRECTION ( 'NONE',  ( -0.9913301211009810654, 0.1313947906041722236, 0.000000000000000000 ) ) ;
#16504=AXIS2_PLACEMENT_3D ( 'NONE', #11184, #6, #7410 ) ;
#16506=EDGE_CURVE ( 'NONE', #1409, #15508, #1354, .T. ) ;
#16508=EDGE_CURVE ( 'NONE', #14186, #9926, #21209, .T. ) ;
#16509=AXIS2_PLACEMENT_3D ( 'NONE', #17087, #22591, #21006 ) ;
#16524=DIRECTION ( 'NONE',  ( 1.000000000000000000, -4.625929269271486900E-15, 0.000000000000000000 ) ) ;
#16542=AXIS2_PLACEMENT_3D ( 'NONE', #16780, #9449, #15309 ) ;
#16545=DIRECTION ( 'NONE',  ( 1.000000000000000000, 0.000000000000000000, -0.000000000000000000 ) ) ;
#16546=DIRECTION ( 'NONE',  ( 0.1313947906041722513, -0.9913301211009810654, 0.000000000000000000 ) ) ;
#16550=EDGE_CURVE ( 'NONE', #18498, #3705, #10303, .T. ) ;
#16562=ORIENTED_EDGE ( 'NONE', *, *, #6050, .F. ) ;
#16567=DIRECTION ( 'NONE',  ( -0.000000000000000000, 0.000000000000000000, -1.000000000000000000 ) ) ;
#16568=VECTOR ( 'NONE', #9623, 1000.000000000000000 ) ;
#16582=DIRECTION ( 'NONE',  ( 0.000000000000000000, 0.000000000000000000, 1.000000000000000000 ) ) ;
#16587=EDGE_CURVE ( 'NONE', #23300, #11051, #4071, .T. ) ;
#16589=AXIS2_PLACEMENT_3D ( 'NONE', #13365, #4110, #15300 ) ;
#16613=EDGE_CURVE ( 'NONE', #1596, #9356, #20434, .T. ) ;
#16618=CYLINDRICAL_SURFACE ( 'NONE', #23494, 5.099999999999996980 ) ;
#16624=DIRECTION ( 'NONE',  ( -0.7071067811865660024, 0.000000000000000000, -0.7071067811865291430 ) ) ;
#16625=DIRECTION ( 'NONE',  ( -0.000000000000000000, 0.000000000000000000, -1.000000000000000000 ) ) ;
#16626=LINE ( 'NONE', #22245, #4548 ) ;
#16630=ORIENTED_EDGE ( 'NONE', *, *, #15331, .F. ) ;
#16641=DIRECTION ( 'NONE',  ( -0.8757121056631633760, -0.4828336235133056653, 0.000000000000000000 ) ) ;
#16659=SHAPE_DEFINITION_REPRESENTATION ( #7621, #19247 ) ;
#16675=CARTESIAN_POINT ( 'NONE',  ( -0.9830802669677229932, 45.00000000000000000, 0.000000000000000000 ) ) ;
#16677=CARTESIAN_POINT ( 'NONE',  ( -27.70933665152131198, 40.41277845351217479, 12.00000000000000000 ) ) ;
#16683=CARTESIAN_POINT ( 'NONE',  ( -31.10231664966676846, -45.36128193761570770, 11.00000000000000000 ) ) ;
#16690=CONICAL_SURFACE ( 'NONE', #10799, 2.024999999999999911, 0.7853981633974743692 ) ;
#16702=CARTESIAN_POINT ( 'NONE',  ( -29.00000000000000000, -29.49999999999999645, 12.00000000000000000 ) ) ;
#16703=CYLINDRICAL_SURFACE ( 'NONE', #118, 20.85000000000000142 ) ;
#16708=ORIENTED_EDGE ( 'NONE', *, *, #21568, .T. ) ;
#16711=ORIENTED_EDGE ( 'NONE', *, *, #10968, .T. ) ;
#16752=CARTESIAN_POINT ( 'NONE',  ( 41.00000000000000000, 0.000000000000000000, 12.00000000000000000 ) ) ;
#16766=ORIENTED_EDGE ( 'NONE', *, *, #7085, .T. ) ;
#16771=FACE_OUTER_BOUND ( 'NONE', #10514, .T. ) ;
#16773=ORIENTED_EDGE ( 'NONE', *, *, #2974, .F. ) ;
#16779=CARTESIAN_POINT ( 'NONE',  ( -41.00000000000000000, 26.23076770084981391, 12.00000000000000000 ) ) ;
#16780=CARTESIAN_POINT ( 'NONE',  ( 29.00000000000000000, -29.50000000000000355, 11.50000000000000000 ) ) ;
#16785=EDGE_CURVE ( 'NONE', #18828, #3216, #6875, .T. ) ;
#16791=EDGE_CURVE ( 'NONE', #21962, #4241, #8728, .T. ) ;
#16794=EDGE_CURVE ( 'NONE', #19325, #20363, #5656, .T. ) ;
#16795=DIRECTION ( 'NONE',  ( 0.000000000000000000, 0.000000000000000000, -1.000000000000000000 ) ) ;
#16796=CARTESIAN_POINT ( 'NONE',  ( -42.00000000000000711, 26.82133436441678498, 11.00000000000000000 ) ) ;
#16798=LINE ( 'NONE', #5730, #1262 ) ;
#16802=CARTESIAN_POINT ( 'NONE',  ( -29.00000000000000000, 29.49999999999999645, 11.50000000000000000 ) ) ;
#16813=CARTESIAN_POINT ( 'NONE',  ( 39.00000000000000000, 28.80990663662251805, 11.00000000000000000 ) ) ;
#16821=EDGE_CURVE ( 'NONE', #2607, #14074, #16255, .T. ) ;
#16826=EDGE_LOOP ( 'NONE', ( #792, #19587, #5744, #13041 ) ) ;
#16827=CARTESIAN_POINT ( 'NONE',  ( 33.99999999999998579, -5.000000000000013323, 10.49999999999999822 ) ) ;
#16828=DIRECTION ( 'NONE',  ( 0.000000000000000000, -0.000000000000000000, -1.000000000000000000 ) ) ;
#16829=VERTEX_POINT ( 'NONE', #16827 ) ;
#16832=AXIS2_PLACEMENT_3D ( 'NONE', #17661, #10564, #8390 ) ;
#16835=VECTOR ( 'NONE', #12545, 1000.000000000000000 ) ;
#16839=DIRECTION ( 'NONE',  ( 1.000000000000000000, 0.000000000000000000, 0.000000000000000000 ) ) ;
#16840=AXIS2_PLACEMENT_3D ( 'NONE', #11589, #17086, #2452 ) ;
#16844=CARTESIAN_POINT ( 'NONE',  ( -3.008080266967722682, 45.00000000000000000, 0.000000000000000000 ) ) ;
#16851=EDGE_LOOP ( 'NONE', ( #14131, #15655 ) ) ;
#16855=ORIENTED_EDGE ( 'NONE', *, *, #16439, .F. ) ;
#16859=CONICAL_SURFACE ( 'NONE', #20009, 2.024999999999999911, 0.7853981633974743692 ) ;
#16860=CIRCLE ( 'NONE', #9450, 2.000000000000000000 ) ;
#16877=EDGE_CURVE ( 'NONE', #11051, #2739, #2411, .T. ) ;
#16881=VERTEX_POINT ( 'NONE', #15574 ) ;
#16885=AXIS2_PLACEMENT_3D ( 'NONE', #12465, #6754, #23474 ) ;
#16894=LINE ( 'NONE', #209, #5244 ) ;
#16897=LINE ( 'NONE', #20330, #7184 ) ;
#16907=CARTESIAN_POINT ( 'NONE',  ( 30.44534269664590553, 40.40463133211080304, 0.000000000000000000 ) ) ;
#16914=ADVANCED_FACE ( 'NONE', ( #2664 ), #6034, .T. ) ;
#16919=ORIENTED_EDGE ( 'NONE', *, *, #20282, .T. ) ;
#16926=AXIS2_PLACEMENT_3D ( 'NONE', #20699, #7857, #15181 ) ;
#16927=CIRCLE ( 'NONE', #3686, 1.000000000000000888 ) ;
#16941=ADVANCED_FACE ( 'NONE', ( #21211 ), #21340, .T. ) ;
#16943=ADVANCED_FACE ( 'NONE', ( #19390 ), #3307, .T. ) ;
#16962=ORIENTED_EDGE ( 'NONE', *, *, #20182, .T. ) ;
#16970=CARTESIAN_POINT ( 'NONE',  ( -21.84999999999999787, 0.000000000000000000, 12.00000000000000000 ) ) ;
#16972=CARTESIAN_POINT ( 'NONE',  ( -2.983080266967717442, 45.00000000000000000, 0.02500000000000418554 ) ) ;
#16973=ORIENTED_EDGE ( 'NONE', *, *, #3345, .T. ) ;
#16980=FACE_OUTER_BOUND ( 'NONE', #15517, .T. ) ;
#16988=ORIENTED_EDGE ( 'NONE', *, *, #10211, .T. ) ;
#16997=AXIS2_PLACEMENT_3D ( 'NONE', #17257, #9682, #7843 ) ;
#16998=EDGE_CURVE ( 'NONE', #16379, #21962, #20469, .T. ) ;
#17000=CARTESIAN_POINT ( 'NONE',  ( -29.00000000000000000, -3.851859888774471706E-31, 10.49999999999999822 ) ) ;
#17003=CARTESIAN_POINT ( 'NONE',  ( -31.10231664966676846, 45.36128193761570770, 11.00000000000000000 ) ) ;
#17005=ORIENTED_EDGE ( 'NONE', *, *, #320, .T. ) ;
#17015=ORIENTED_EDGE ( 'NONE', *, *, #17396, .F. ) ;
#17016=DIRECTION ( 'NONE',  ( 1.000000000000000000, 0.000000000000000000, 0.000000000000000000 ) ) ;
#17025=ADVANCED_FACE ( 'NONE', ( #17148 ), #13377, .F. ) ;
#17030=DIRECTION ( 'NONE',  ( -0.000000000000000000, -0.000000000000000000, -1.000000000000000000 ) ) ;
#17037=ORIENTED_EDGE ( 'NONE', *, *, #4799, .F. ) ;
#17040=EDGE_LOOP ( 'NONE', ( #4757, #2017, #19911, #13709 ) ) ;
#17043=DIRECTION ( 'NONE',  ( 1.000000000000000000, 0.000000000000000000, 0.000000000000000000 ) ) ;
#17045=CIRCLE ( 'NONE', #23317, 10.00000000000000533 ) ;
#17046=ADVANCED_FACE ( 'NONE', ( #18638 ), #13824, .T. ) ;
#17063=ORIENTED_EDGE ( 'NONE', *, *, #5132, .T. ) ;
#17066=PLANE ( 'NONE',  #14145 ) ;
#17070=CARTESIAN_POINT ( 'NONE',  ( 20.85000000000000497, 16.67999999999999972, 13.00000000000000178 ) ) ;
#17076=EDGE_CURVE ( 'NONE', #21352, #3705, #981, .T. ) ;
#17083=CYLINDRICAL_SURFACE ( 'NONE', #18264, 1.000000000000000888 ) ;
#17084=FACE_OUTER_BOUND ( 'NONE', #7902, .T. ) ;
#17086=DIRECTION ( 'NONE',  ( 0.000000000000000000, -0.000000000000000000, -1.000000000000000000 ) ) ;
#17087=CARTESIAN_POINT ( 'NONE',  ( -29.00000000000000000, -29.49999999999999645, 11.50000000000000000 ) ) ;
#17096=CARTESIAN_POINT ( 'NONE',  ( 23.90000000000000568, 29.50000000000000355, 11.50000000000000000 ) ) ;
#17107=ORIENTED_EDGE ( 'NONE', *, *, #23440, .T. ) ;
#17110=EDGE_LOOP ( 'NONE', ( #6813, #2228, #19398, #11733 ) ) ;
#17117=DIRECTION ( 'NONE',  ( 0.000000000000000000, -0.000000000000000000, -1.000000000000000000 ) ) ;
#17123=VERTEX_POINT ( 'NONE', #2523 ) ;
#17139=DIRECTION ( 'NONE',  ( 0.000000000000000000, 0.000000000000000000, 1.000000000000000000 ) ) ;
#17143=AXIS2_PLACEMENT_3D ( 'NONE', #13037, #22110, #10840 ) ;
#17145=DIRECTION ( 'NONE',  ( -1.000000000000000000, 0.000000000000000000, 0.000000000000000000 ) ) ;
#17147=CARTESIAN_POINT ( 'NONE',  ( -29.00000000000000000, 29.49999999999999645, 12.00000000000000000 ) ) ;
#17148=FACE_OUTER_BOUND ( 'NONE', #10093, .T. ) ;
#17150=EDGE_CURVE ( 'NONE', #12632, #13595, #23186, .T. ) ;
#17165=CARTESIAN_POINT ( 'NONE',  ( -42.00000000000000000, 6.000000000000000888, 12.00000000000000000 ) ) ;
#17169=CARTESIAN_POINT ( 'NONE',  ( -41.58578643762692195, -26.57671364288190574, 12.00000000000000355 ) ) ;
#17170=EDGE_LOOP ( 'NONE', ( #16855, #20572, #3514, #2577, #7475 ) ) ;
#17174=ORIENTED_EDGE ( 'NONE', *, *, #6648, .T. ) ;
#17176=DIRECTION ( 'NONE',  ( -0.000000000000000000, -0.000000000000000000, -1.000000000000000000 ) ) ;
#17188=VECTOR ( 'NONE', #18231, 1000.000000000000000 ) ;
#17189=CARTESIAN_POINT ( 'NONE',  ( 31.10231664966676846, 45.36128193761570770, 11.00000000000000000 ) ) ;
#17195=CARTESIAN_POINT ( 'NONE',  ( 41.00000000000000000, 4.999999999999986677, 11.00000000000000000 ) ) ;
#17209=DIRECTION ( 'NONE',  ( 1.000000000000000000, 0.000000000000000000, 0.000000000000000000 ) ) ;
#17214=EDGE_CURVE ( 'NONE', #758, #22790, #17778, .T. ) ;
#17216=DIRECTION ( 'NONE',  ( 1.000000000000000000, 0.000000000000000000, -0.000000000000000000 ) ) ;
#17227=FACE_BOUND ( 'NONE', #6375, .T. ) ;
#17229=ORIENTED_EDGE ( 'NONE', *, *, #10741, .T. ) ;
#17237=DIRECTION ( 'NONE',  ( -0.000000000000000000, -0.000000000000000000, -1.000000000000000000 ) ) ;
#17249=AXIS2_PLACEMENT_3D ( 'NONE', #17947, #20257, #6848 ) ;
#17251=AXIS2_PLACEMENT_3D ( 'NONE', #5178, #12734, #21666 ) ;
#17257=CARTESIAN_POINT ( 'NONE',  ( 41.50000000000000000, -28.80990663662250739, 12.00000000000000000 ) ) ;
#17274=AXIS2_PLACEMENT_3D ( 'NONE', #17980, #1269, #12467 ) ;
#17280=EDGE_LOOP ( 'NONE', ( #2167, #9185, #2484, #1102 ) ) ;
#17287=CARTESIAN_POINT ( 'NONE',  ( -28.27483331787888687, 41.23752903419610050, 11.00000000000000000 ) ) ;
#17294=AXIS2_PLACEMENT_3D ( 'NONE', #13964, #21409, #4694 ) ;
#17298=DIRECTION ( 'NONE',  ( 0.000000000000000000, 1.000000000000000000, 0.000000000000000000 ) ) ;
#17300=VECTOR ( 'NONE', #11301, 1000.000000000000000 ) ;
#17301=EDGE_CURVE ( 'NONE', #21814, #20489, #2479, .T. ) ;
#17304=CARTESIAN_POINT ( 'NONE',  ( -29.00000000000000000, 29.49999999999999645, 11.50000000000000000 ) ) ;
#17306=EDGE_CURVE ( 'NONE', #19937, #20363, #17687, .T. ) ;
#17320=FACE_OUTER_BOUND ( 'NONE', #23168, .T. ) ;
#17323=CIRCLE ( 'NONE', #16542, 5.099999999999996980 ) ;
#17327=DIRECTION ( 'NONE',  ( 0.8571673007021116675, 1.049727191138617833E-16, -0.5150380749100552658 ) ) ;
#17348=DIRECTION ( 'NONE',  ( 0.000000000000000000, 0.000000000000000000, 1.000000000000000000 ) ) ;
#17362=PLANE ( 'NONE',  #5091 ) ;
#17368=CARTESIAN_POINT ( 'NONE',  ( -34.00000000000000000, -4.999999999999999112, 9.500000000000000000 ) ) ;
#17371=ORIENTED_EDGE ( 'NONE', *, *, #22302, .T. ) ;
#17372=CARTESIAN_POINT ( 'NONE',  ( -34.10000000000000142, 29.49999999999999645, 11.50000000000000000 ) ) ;
#17391=CIRCLE ( 'NONE', #16997, 2.500000000000002220 ) ;
#17396=EDGE_CURVE ( 'NONE', #12189, #19800, #8725, .T. ) ;
#17397=EDGE_CURVE ( 'NONE', #8229, #16379, #3324, .T. ) ;
#17404=LINE ( 'NONE', #22779, #14457 ) ;
#17411=ORIENTED_EDGE ( 'NONE', *, *, #23341, .T. ) ;
#17414=VERTEX_POINT ( 'NONE', #5321 ) ;
#17417=DIRECTION ( 'NONE',  ( -0.000000000000000000, -0.000000000000000000, 1.000000000000000000 ) ) ;
#17420=CARTESIAN_POINT ( 'NONE',  ( -39.00000000000000711, -29.49999999999999645, 12.00000000000000000 ) ) ;
#17423=DIRECTION ( 'NONE',  ( -0.000000000000000000, 0.000000000000000000, 1.000000000000000000 ) ) ;
#17429=LINE ( 'NONE', #6584, #7135 ) ;
#17440=CARTESIAN_POINT ( 'NONE',  ( 28.27483331787888332, -41.23752903419610050, 0.000000000000000000 ) ) ;
#17443=DIRECTION ( 'NONE',  ( -0.000000000000000000, 0.000000000000000000, 1.000000000000000000 ) ) ;
#17445=EDGE_CURVE ( 'NONE', #11051, #2256, #6388, .T. ) ;
#17452=CIRCLE ( 'NONE', #10032, 5.099999999999996980 ) ;
#17453=CARTESIAN_POINT ( 'NONE',  ( -29.00000000000000000, 29.49999999999999645, 0.000000000000000000 ) ) ;
#17455=CYLINDRICAL_SURFACE ( 'NONE', #4701, 1.000000000000000888 ) ;
#17462=FACE_OUTER_BOUND ( 'NONE', #12103, .T. ) ;
#17472=VERTEX_POINT ( 'NONE', #24090 ) ;
#17478=DIRECTION ( 'NONE',  ( -1.000000000000000000, -2.600433232233976523E-16, -0.000000000000000000 ) ) ;
#17482=DIRECTION ( 'NONE',  ( -0.000000000000000000, -0.000000000000000000, -1.000000000000000000 ) ) ;
#17485=ORIENTED_EDGE ( 'NONE', *, *, #18500, .T. ) ;
#17492=ORIENTED_EDGE ( 'NONE', *, *, #6182, .F. ) ;
#17493=ADVANCED_FACE ( 'NONE', ( #13103 ), #12976, .F. ) ;
#17494=AXIS2_PLACEMENT_3D ( 'NONE', #12897, #18534, #11282 ) ;
#17501=ORIENTED_EDGE ( 'NONE', *, *, #21653, .F. ) ;
#17506=DIRECTION ( 'NONE',  ( -0.000000000000000000, -0.000000000000000000, -1.000000000000000000 ) ) ;
#17528=CARTESIAN_POINT ( 'NONE',  ( 33.99999999999998579, -6.000000000000013323, 12.00000000000000000 ) ) ;
#17534=VERTEX_POINT ( 'NONE', #13337 ) ;
#17541=EDGE_CURVE ( 'NONE', #5671, #12632, #18609, .T. ) ;
#17547=VECTOR ( 'NONE', #7689, 1000.000000000000000 ) ;
#17549=SPHERICAL_SURFACE ( 'NONE', #4680, 1.000000000000000000 ) ;
#17560=ORIENTED_EDGE ( 'NONE', *, *, #10304, .T. ) ;
#17577=DIRECTION ( 'NONE',  ( -1.000000000000000000, 0.000000000000000000, 0.000000000000000000 ) ) ;
#17586=ORIENTED_EDGE ( 'NONE', *, *, #21530, .F. ) ;
#17591=ORIENTED_EDGE ( 'NONE', *, *, #1717, .T. ) ;
#17594=EDGE_CURVE ( 'NONE', #9993, #15508, #20033, .T. ) ;
#17597=PLANE ( 'NONE',  #18414 ) ;
#17608=ORIENTED_EDGE ( 'NONE', *, *, #23483, .T. ) ;
#17612=AXIS2_PLACEMENT_3D ( 'NONE', #15385, #6132, #17577 ) ;
#17618=FACE_OUTER_BOUND ( 'NONE', #2730, .T. ) ;
#17623=VECTOR ( 'NONE', #23722, 1000.000000000000000 ) ;
#17628=EDGE_CURVE ( 'NONE', #9926, #14186, #21208, .T. ) ;
#17637=AXIS2_PLACEMENT_3D ( 'NONE', #9996, #2947, #15604 ) ;
#17639=AXIS2_PLACEMENT_3D ( 'NONE', #2091, #9517, #7564 ) ;
#17642=VERTEX_POINT ( 'NONE', #17372 ) ;
#17646=ORIENTED_EDGE ( 'NONE', *, *, #13348, .T. ) ;
#17661=CARTESIAN_POINT ( 'NONE',  ( 33.99999999999998579, 4.999999999999985789, 9.500000000000000000 ) ) ;
#17665=CARTESIAN_POINT ( 'NONE',  ( -37.00000000000000711, 29.49999999999999645, 11.50000000000000000 ) ) ;
#17667=EDGE_LOOP ( 'NONE', ( #4457, #1502, #8269, #17174 ) ) ;
#17668=FACE_OUTER_BOUND ( 'NONE', #17280, .T. ) ;
#17670=CIRCLE ( 'NONE', #12586, 4.000000000000000000 ) ;
#17676=ORIENTED_EDGE ( 'NONE', *, *, #4742, .F. ) ;
#17677=CIRCLE ( 'NONE', #23528, 0.9999999999999994449 ) ;
#17685=AXIS2_PLACEMENT_3D ( 'NONE', #7429, #23623, #14318 ) ;
#17687=CIRCLE ( 'NONE', #9102, 1.000000000000000888 ) ;
#17709=CYLINDRICAL_SURFACE ( 'NONE', #2904, 4.999999999999997335 ) ;
#17714=DIRECTION ( 'NONE',  ( -0.4828336235133043330, -0.8757121056631641531, 0.000000000000000000 ) ) ;
#17723=AXIS2_PLACEMENT_3D ( 'NONE', #225, #3982, #11163 ) ;
#17729=DIRECTION ( 'NONE',  ( 1.000000000000000000, 0.000000000000000000, 0.000000000000000000 ) ) ;
#17748=ORIENTED_EDGE ( 'NONE', *, *, #8058, .T. ) ;
#17758=DIRECTION ( 'NONE',  ( -1.000000000000000000, 0.000000000000000000, 0.000000000000000000 ) ) ;
#17759=ADVANCED_FACE ( 'NONE', ( #6528 ), #4455, .F. ) ;
#17760=DIRECTION ( 'NONE',  ( -1.000000000000000000, 0.000000000000000000, 0.000000000000000000 ) ) ;
#17761=ORIENTED_EDGE ( 'NONE', *, *, #9747, .F. ) ;
#17764=AXIS2_PLACEMENT_3D ( 'NONE', #6573, #4872, #4626 ) ;
#17772=CARTESIAN_POINT ( 'NONE',  ( 41.00000000000000000, 5.999999999999986677, 11.00000000000000000 ) ) ;
#17773=AXIS2_PLACEMENT_3D ( 'NONE', #8717, #3008, #16166 ) ;
#17774=FACE_OUTER_BOUND ( 'NONE', #2246, .T. ) ;
#17778=LINE ( 'NONE', #13875, #11422 ) ;
#17782=ORIENTED_EDGE ( 'NONE', *, *, #3786, .F. ) ;
#17784=AXIS2_PLACEMENT_3D ( 'NONE', #7489, #11151, #437 ) ;
#17785=ORIENTED_EDGE ( 'NONE', *, *, #16794, .T. ) ;
#17789=AXIS2_PLACEMENT_3D ( 'NONE', #827, #9954, #4740 ) ;
#17792=DIRECTION ( 'NONE',  ( 1.000000000000000000, 0.000000000000000000, 0.000000000000000000 ) ) ;
#17795=AXIS2_PLACEMENT_3D ( 'NONE', #13815, #12212, #21629 ) ;
#17803=AXIS2_PLACEMENT_3D ( 'NONE', #8213, #21050, #22898 ) ;
#17804=CARTESIAN_POINT ( 'NONE',  ( -34.00000000000000000, -3.851859888774471706E-31, 10.49999999999999822 ) ) ;
#17808=CARTESIAN_POINT ( 'NONE',  ( 34.10000000000000142, -29.50000000000000355, 0.000000000000000000 ) ) ;
#17831=ORIENTED_EDGE ( 'NONE', *, *, #19994, .F. ) ;
#17835=FACE_OUTER_BOUND ( 'NONE', #7351, .T. ) ;
#17836=CARTESIAN_POINT ( 'NONE',  ( 33.99999999999998579, 3.999999999999985345, 10.49999999999999822 ) ) ;
#17842=FACE_OUTER_BOUND ( 'NONE', #17170, .T. ) ;
#17846=DIRECTION ( 'NONE',  ( 1.000000000000000000, 0.000000000000000000, 0.000000000000000000 ) ) ;
#17847=EDGE_CURVE ( 'NONE', #21048, #7050, #9877, .T. ) ;
#17863=CARTESIAN_POINT ( 'NONE',  ( 33.99999999999998579, -4.000000000000013323, 10.49999999999999822 ) ) ;
#17867=CARTESIAN_POINT ( 'NONE',  ( -30.44534269664590553, -40.40463133211081015, 0.000000000000000000 ) ) ;
#17870=FACE_OUTER_BOUND ( 'NONE', #20397, .T. ) ;
#17875=AXIS2_PLACEMENT_3D ( 'NONE', #8922, #1615, #12711 ) ;
#17891=EDGE_CURVE ( 'NONE', #9763, #22408, #7543, .T. ) ;
#17907=DIRECTION ( 'NONE',  ( -0.000000000000000000, 0.000000000000000000, 1.000000000000000000 ) ) ;
#17917=CIRCLE ( 'NONE', #9313, 1.000000000000000000 ) ;
#17935=VECTOR ( 'NONE', #4983, 1000.000000000000000 ) ;
#17947=CARTESIAN_POINT ( 'NONE',  ( -39.00000000000000711, 29.49999999999999645, 11.00000000000000000 ) ) ;
#17950=DIRECTION ( 'NONE',  ( -0.000000000000000000, -0.000000000000000000, -1.000000000000000000 ) ) ;
#17952=ORIENTED_EDGE ( 'NONE', *, *, #3237, .F. ) ;
#17954=DIRECTION ( 'NONE',  ( -0.000000000000000000, 0.000000000000000000, 1.000000000000000000 ) ) ;
#17958=CARTESIAN_POINT ( 'NONE',  ( 0.000000000000000000, -45.00000000000000000, 0.000000000000000000 ) ) ;
#17974=EDGE_CURVE ( 'NONE', #5826, #9925, #18694, .T. ) ;
#17980=CARTESIAN_POINT ( 'NONE',  ( 2.454813078130514813E-15, 16.67999999999999972, 13.50000000000000178 ) ) ;
#17989=DIRECTION ( 'NONE',  ( -1.000000000000000000, 0.000000000000000000, 0.000000000000000000 ) ) ;
#17992=DIRECTION ( 'NONE',  ( -1.000000000000000000, 0.000000000000000000, 0.000000000000000000 ) ) ;
#18003=EDGE_CURVE ( 'NONE', #2256, #14909, #288, .T. ) ;
#18007=CARTESIAN_POINT ( 'NONE',  ( -31.10231664966676846, -45.36128193761570770, 12.00000000000000000 ) ) ;
#18009=DIRECTION ( 'NONE',  ( 0.7071067811865660024, 8.659560562355159656E-17, -0.7071067811865291430 ) ) ;
#18015=AXIS2_PLACEMENT_3D ( 'NONE', #17863, #21518, #21646 ) ;
#18020=CARTESIAN_POINT ( 'NONE',  ( 41.00000000000000000, -6.000000000000015099, 10.49999999999999822 ) ) ;
#18025=DIRECTION ( 'NONE',  ( 1.000000000000000000, 0.000000000000000000, 0.000000000000000000 ) ) ;
#18029=CIRCLE ( 'NONE', #13321, 20.85000000000000142 ) ;
#18034=PLANE ( 'NONE',  #19192 ) ;
#18036=DIRECTION ( 'NONE',  ( 1.000000000000000000, 0.000000000000000000, 0.000000000000000000 ) ) ;
#18054=EDGE_CURVE ( 'NONE', #10216, #1666, #2594, .T. ) ;
#18055=CIRCLE ( 'NONE', #1680, 4.999999999999997335 ) ;
#18058=AXIS2_PLACEMENT_3D ( 'NONE', #22584, #5865, #2082 ) ;
#18061=DIRECTION ( 'NONE',  ( -0.000000000000000000, -0.000000000000000000, -1.000000000000000000 ) ) ;
#18062=ADVANCED_FACE ( 'NONE', ( #17462 ), #2337, .F. ) ;
#18064=ORIENTED_EDGE ( 'NONE', *, *, #10738, .F. ) ;
#18069=CARTESIAN_POINT ( 'NONE',  ( 23.90000000000000568, -29.50000000000000355, 12.00000000000000000 ) ) ;
#18071=CARTESIAN_POINT ( 'NONE',  ( -41.00000000000000000, -6.000000000000000888, 10.49999999999999822 ) ) ;
#18075=DIRECTION ( 'NONE',  ( -0.8571673007021116675, 0.000000000000000000, -0.5150380749100552658 ) ) ;
#18079=CIRCLE ( 'NONE', #6770, 1.000000000000000888 ) ;
#18086=LINE ( 'NONE', #11310, #20159 ) ;
#18087=DIRECTION ( 'NONE',  ( 0.000000000000000000, 0.000000000000000000, 1.000000000000000000 ) ) ;
#18098=VECTOR ( 'NONE', #5268, 1000.000000000000000 ) ;
#18099=DIRECTION ( 'NONE',  ( 1.000000000000000000, 0.000000000000000000, -0.000000000000000000 ) ) ;
#18115=ADVANCED_FACE ( 'NONE', ( #1341 ), #16374, .T. ) ;
#18129=ORIENTED_EDGE ( 'NONE', *, *, #22889, .F. ) ;
#18146=EDGE_CURVE ( 'NONE', #21867, #21197, #20292, .T. ) ;
#18148=ORIENTED_EDGE ( 'NONE', *, *, #8013, .T. ) ;
#18149=ORIENTED_EDGE ( 'NONE', *, *, #23260, .F. ) ;
#18151=DIRECTION ( 'NONE',  ( 1.000000000000000000, 0.000000000000000000, 0.000000000000000000 ) ) ;
#18171=VECTOR ( 'NONE', #13122, 1000.000000000000227 ) ;
#18180=ORIENTED_EDGE ( 'NONE', *, *, #817, .T. ) ;
#18183=CIRCLE ( 'NONE', #8427, 1.000000000000000888 ) ;
#18187=CARTESIAN_POINT ( 'NONE',  ( 1.016919733032271456, 45.00000000000000000, 0.000000000000000000 ) ) ;
#18203=ORIENTED_EDGE ( 'NONE', *, *, #6648, .F. ) ;
#18211=DIRECTION ( 'NONE',  ( 0.000000000000000000, -0.000000000000000000, -1.000000000000000000 ) ) ;
#18212=EDGE_CURVE ( 'NONE', #8169, #21352, #10906, .T. ) ;
#18222=ORIENTED_EDGE ( 'NONE', *, *, #3438, .F. ) ;
#18231=DIRECTION ( 'NONE',  ( 0.000000000000000000, -1.000000000000000000, 0.000000000000000000 ) ) ;
#18232=ORIENTED_EDGE ( 'NONE', *, *, #6799, .T. ) ;
#18234=ORIENTED_EDGE ( 'NONE', *, *, #5463, .T. ) ;
#18236=DIRECTION ( 'NONE',  ( 0.000000000000000000, 0.000000000000000000, 1.000000000000000000 ) ) ;
#18237=CARTESIAN_POINT ( 'NONE',  ( 31.10231664966676846, 45.36128193761570770, 11.00000000000000000 ) ) ;
#18239=VERTEX_POINT ( 'NONE', #14366 ) ;
#18243=CARTESIAN_POINT ( 'NONE',  ( -34.00000000000000000, -3.851859888774471706E-31, 12.00000000000000000 ) ) ;
#18247=AXIS2_PLACEMENT_3D ( 'NONE', #8864, #16304, #22181 ) ;
#18251=EDGE_CURVE ( 'NONE', #16231, #10954, #7044, .T. ) ;
#18253=ADVANCED_FACE ( 'NONE', ( #12656 ), #8881, .F. ) ;
#18261=EDGE_LOOP ( 'NONE', ( #21708, #643, #1544 ) ) ;
#18264=AXIS2_PLACEMENT_3D ( 'NONE', #9512, #22585, #385 ) ;
#18280=ADVANCED_FACE ( 'NONE', ( #10816 ), #13268, .T. ) ;
#18282=DIRECTION ( 'NONE',  ( -0.000000000000000000, 1.000000000000000000, -0.000000000000000000 ) ) ;
#18285=DIRECTION ( 'NONE',  ( 1.000000000000000000, 0.000000000000000000, 0.000000000000000000 ) ) ;
#18295=CARTESIAN_POINT ( 'NONE',  ( -42.00000000000000000, 0.000000000000000000, 0.000000000000000000 ) ) ;
#18306=EDGE_CURVE ( 'NONE', #20942, #10396, #15600, .T. ) ;
#18316=DIRECTION ( 'NONE',  ( -0.000000000000000000, -0.000000000000000000, -1.000000000000000000 ) ) ;
#18323=FACE_OUTER_BOUND ( 'NONE', #2164, .T. ) ;
#18338=CARTESIAN_POINT ( 'NONE',  ( 33.99999999999998579, -1.387778780781445676E-14, 9.500000000000000000 ) ) ;
#18355=CYLINDRICAL_SURFACE ( 'NONE', #5060, 8.000000000000003553 ) ;
#18357=DIRECTION ( 'NONE',  ( 1.000000000000000000, 0.000000000000000000, 0.000000000000000000 ) ) ;
#18360=CARTESIAN_POINT ( 'NONE',  ( -41.50000000000000000, 28.80990663662250739, 11.00000000000000000 ) ) ;
#18361=DIRECTION ( 'NONE',  ( -0.000000000000000000, -0.000000000000000000, -1.000000000000000000 ) ) ;
#18386=DIRECTION ( 'NONE',  ( 0.000000000000000000, -1.000000000000000000, 0.000000000000000000 ) ) ;
#18414=AXIS2_PLACEMENT_3D ( 'NONE', #20919, #19337, #6523 ) ;
#18424=ORIENTED_EDGE ( 'NONE', *, *, #8706, .T. ) ;
#18429=AXIS2_PLACEMENT_3D ( 'NONE', #20659, #18830, #20049 ) ;
#18435=EDGE_CURVE ( 'NONE', #2518, #5912, #4727, .T. ) ;
#18438=LINE ( 'NONE', #1729, #2560 ) ;
#18441=ADVANCED_FACE ( 'NONE', ( #4497 ), #15683, .F. ) ;
#18448=CIRCLE ( 'NONE', #7898, 1.000000000000000888 ) ;
#18454=ORIENTED_EDGE ( 'NONE', *, *, #16791, .T. ) ;
#18461=CARTESIAN_POINT ( 'NONE',  ( 40.29291594121673370, -26.62062637246459218, 12.00000000000000000 ) ) ;
#18467=AXIS2_PLACEMENT_3D ( 'NONE', #8349, #23266, #17758 ) ;
#18492=ORIENTED_EDGE ( 'NONE', *, *, #15051, .F. ) ;
#18498=VERTEX_POINT ( 'NONE', #10063 ) ;
#18500=EDGE_CURVE ( 'NONE', #13857, #19153, #7808, .T. ) ;
#18506=CARTESIAN_POINT ( 'NONE',  ( 1.016919733032271456, 45.00000000000000000, 3.000000000000002665 ) ) ;
#18516=CARTESIAN_POINT ( 'NONE',  ( 23.90000000000000568, 29.50000000000000355, 0.000000000000000000 ) ) ;
#18522=DIRECTION ( 'NONE',  ( -0.8571673007021116675, 0.000000000000000000, -0.5150380749100552658 ) ) ;
#18532=ORIENTED_EDGE ( 'NONE', *, *, #155, .T. ) ;
#18534=DIRECTION ( 'NONE',  ( -0.000000000000000000, 0.000000000000000000, 1.000000000000000000 ) ) ;
#18536=ORIENTED_EDGE ( 'NONE', *, *, #4369, .T. ) ;
#18541=DIRECTION ( 'NONE',  ( -0.000000000000000000, -0.000000000000000000, -1.000000000000000000 ) ) ;
#18546=DIRECTION ( 'NONE',  ( 0.000000000000000000, 0.000000000000000000, 1.000000000000000000 ) ) ;
#18547=CARTESIAN_POINT ( 'NONE',  ( 40.00000000000000000, 29.49999999999999645, 12.00000000000000000 ) ) ;
#18555=CARTESIAN_POINT ( 'NONE',  ( -29.00000000000000000, 29.49999999999999645, 12.00000000000000000 ) ) ;
#18556=EDGE_CURVE ( 'NONE', #13716, #19319, #14445, .T. ) ;
#18567=CARTESIAN_POINT ( 'NONE',  ( 29.00000000000000000, -29.50000000000000355, 11.50000000000000000 ) ) ;
#18580=ORIENTED_EDGE ( 'NONE', *, *, #21395, .T. ) ;
#18582=FACE_OUTER_BOUND ( 'NONE', #7678, .T. ) ;
#18585=CARTESIAN_POINT ( 'NONE',  ( -34.00000000000000000, -3.851859888774471706E-31, 9.500000000000000000 ) ) ;
#18586=ORIENTED_EDGE ( 'NONE', *, *, #5840, .F. ) ;
#18589=ADVANCED_FACE ( 'NONE', ( #1274 ), #10764, .T. ) ;
#18604=EDGE_CURVE ( 'NONE', #13932, #12301, #14311, .T. ) ;
#18605=FACE_OUTER_BOUND ( 'NONE', #21446, .T. ) ;
#18608=CARTESIAN_POINT ( 'NONE',  ( -41.00000000000000000, 0.000000000000000000, 11.00000000000000000 ) ) ;
#18609=LINE ( 'NONE', #13471, #23535 ) ;
#18620=ORIENTED_EDGE ( 'NONE', *, *, #1559, .T. ) ;
#18628=ORIENTED_EDGE ( 'NONE', *, *, #12398, .T. ) ;
#18632=ORIENTED_EDGE ( 'NONE', *, *, #5039, .T. ) ;
#18638=FACE_OUTER_BOUND ( 'NONE', #16407, .T. ) ;
#18639=CARTESIAN_POINT ( 'NONE',  ( 21.85000000000000497, 16.67999999999999972, 12.00000000000000000 ) ) ;
#18649=( NAMED_UNIT ( * ) PLANE_ANGLE_UNIT ( ) SI_UNIT ( $, .RADIAN. ) );
#18650=TOROIDAL_SURFACE ( 'NONE', #17875, 2.500000000000001776, 1.000000000000000000 ) ;
#18654=CYLINDRICAL_SURFACE ( 'NONE', #11794, 1.000000000000000888 ) ;
#18659=ORIENTED_EDGE ( 'NONE', *, *, #13476, .T. ) ;
#18670=ORIENTED_EDGE ( 'NONE', *, *, #15051, .T. ) ;
#18674=DIRECTION ( 'NONE',  ( 0.000000000000000000, 1.000000000000000000, -0.000000000000000000 ) ) ;
#18676=LINE ( 'NONE', #22, #9939 ) ;
#18680=ORIENTED_EDGE ( 'NONE', *, *, #13722, .T. ) ;
#18684=ADVANCED_FACE ( 'NONE', ( #6353 ), #23445, .T. ) ;
#18690=DIRECTION ( 'NONE',  ( -1.000000000000000000, 0.000000000000000000, 0.000000000000000000 ) ) ;
#18692=CARTESIAN_POINT ( 'NONE',  ( 0.000000000000000000, 0.000000000000000000, 12.00000000000000000 ) ) ;
#18694=LINE ( 'NONE', #16844, #1954 ) ;
#18697=CARTESIAN_POINT ( 'NONE',  ( -0.9830802669677229932, 45.00000000000000000, 0.02500000000000418554 ) ) ;
#18699=ORIENTED_EDGE ( 'NONE', *, *, #22303, .F. ) ;
#18709=ADVANCED_FACE ( 'NONE', ( #19418 ), #14152, .T. ) ;
#18711=ORIENTED_EDGE ( 'NONE', *, *, #22174, .F. ) ;
#18720=LINE ( 'NONE', #14572, #15815 ) ;
#18727=ORIENTED_EDGE ( 'NONE', *, *, #10473, .F. ) ;
#18734=CARTESIAN_POINT ( 'NONE',  ( -20.99999999999999645, -29.49999999999999645, 11.50000000000000000 ) ) ;
#18745=DIRECTION ( 'NONE',  ( -0.8757121056631633760, -0.4828336235133056653, 1.675165643398955870E-15 ) ) ;
#18757=LINE ( 'NONE', #18295, #13379 ) ;
#18760=CARTESIAN_POINT ( 'NONE',  ( 2.454813078130514813E-15, 16.67999999999999972, 13.00000000000000178 ) ) ;
#18762=ORIENTED_EDGE ( 'NONE', *, *, #22243, .F. ) ;
#18766=CARTESIAN_POINT ( 'NONE',  ( -41.00000000000000000, -6.000000000000000888, 11.00000000000000000 ) ) ;
#18767=DIRECTION ( 'NONE',  ( -0.000000000000000000, -0.000000000000000000, -1.000000000000000000 ) ) ;
#18768=CIRCLE ( 'NONE', #10187, 1.000000000000000888 ) ;
#18775=ORIENTED_EDGE ( 'NONE', *, *, #13568, .T. ) ;
#18780=DIRECTION ( 'NONE',  ( -1.000000000000000000, 0.000000000000000000, 0.000000000000000000 ) ) ;
#18781=AXIS2_PLACEMENT_3D ( 'NONE', #2274, #20694, #9332 ) ;
#18787=DIRECTION ( 'NONE',  ( 1.000000000000000000, 0.000000000000000000, -0.000000000000000000 ) ) ;
#18796=DIRECTION ( 'NONE',  ( -0.000000000000000000, -0.000000000000000000, 1.000000000000000000 ) ) ;
#18804=FACE_OUTER_BOUND ( 'NONE', #21026, .T. ) ;
#18816=FACE_OUTER_BOUND ( 'NONE', #4040, .T. ) ;
#18817=EDGE_LOOP ( 'NONE', ( #15265, #17107, #23720, #4449 ) ) ;
#18819=ADVANCED_FACE ( 'NONE', ( #20147, #6962 ), #11064, .T. ) ;
#18823=DIRECTION ( 'NONE',  ( 0.000000000000000000, 0.000000000000000000, 1.000000000000000000 ) ) ;
#18828=VERTEX_POINT ( 'NONE', #1362 ) ;
#18830=DIRECTION ( 'NONE',  ( -0.000000000000000000, 0.000000000000000000, 1.000000000000000000 ) ) ;
#18838=DIRECTION ( 'NONE',  ( -0.000000000000000000, -0.000000000000000000, 1.000000000000000000 ) ) ;
#18840=ORIENTED_EDGE ( 'NONE', *, *, #5929, .F. ) ;
#18844=ORIENTED_EDGE ( 'NONE', *, *, #10628, .T. ) ;
#18845=CIRCLE ( 'NONE', #8314, 5.099999999999996980 ) ;
#18851=VECTOR ( 'NONE', #7015, 1000.000000000000000 ) ;
#18857=ORIENTED_EDGE ( 'NONE', *, *, #17974, .T. ) ;
#18866=CIRCLE ( 'NONE', #7179, 1.000000000000001998 ) ;
#18887=AXIS2_PLACEMENT_3D ( 'NONE', #11186, #23917, #16582 ) ;
#18888=CARTESIAN_POINT ( 'NONE',  ( 29.00000000000000000, -29.50000000000000355, 11.50000000000000000 ) ) ;
#18901=DIRECTION ( 'NONE',  ( -0.000000000000000000, -0.000000000000000000, -1.000000000000000000 ) ) ;
#18905=EDGE_CURVE ( 'NONE', #15347, #11492, #11327, .T. ) ;
#18908=TOROIDAL_SURFACE ( 'NONE', #13510, 2.500000000000001776, 1.000000000000000000 ) ;
#18917=ORIENTED_EDGE ( 'NONE', *, *, #4742, .T. ) ;
#18930=EDGE_CURVE ( 'NONE', #1666, #17534, #853, .T. ) ;
#18941=DIRECTION ( 'NONE',  ( 0.000000000000000000, 0.000000000000000000, 1.000000000000000000 ) ) ;
#18953=AXIS2_PLACEMENT_3D ( 'NONE', #4772, #8780, #12186 ) ;
#18963=DIRECTION ( 'NONE',  ( -1.000000000000000000, 0.000000000000000000, 0.000000000000000000 ) ) ;
#18973=CYLINDRICAL_SURFACE ( 'NONE', #5634, 1.000000000000000888 ) ;
#18977=CYLINDRICAL_SURFACE ( 'NONE', #20890, 5.099999999999996980 ) ;
#18986=VERTEX_POINT ( 'NONE', #19136 ) ;
#18990=CARTESIAN_POINT ( 'NONE',  ( -29.00000000000000000, -29.49999999999999645, 11.50000000000000000 ) ) ;
#18998=ADVANCED_FACE ( 'NONE', ( #3778 ), #23838, .F. ) ;
#19009=VERTEX_POINT ( 'NONE', #14978 ) ;
#19015=CARTESIAN_POINT ( 'NONE',  ( 20.85000000000000497, 16.67999999999999972, 13.50000000000000178 ) ) ;
#19028=EDGE_CURVE ( 'NONE', #12778, #16881, #16049, .T. ) ;
#19029=DIRECTION ( 'NONE',  ( 0.000000000000000000, 0.000000000000000000, 1.000000000000000000 ) ) ;
#19031=EDGE_CURVE ( 'NONE', #2772, #20942, #21587, .T. ) ;
#19032=CARTESIAN_POINT ( 'NONE',  ( 2.454813078130514813E-15, -16.67999999999999972, 14.50000000000000000 ) ) ;
#19037=AXIS2_PLACEMENT_3D ( 'NONE', #18071, #21615, #23569 ) ;
#19040=FACE_OUTER_BOUND ( 'NONE', #6385, .T. ) ;
#19042=FACE_OUTER_BOUND ( 'NONE', #18817, .T. ) ;
#19045=DIRECTION ( 'NONE',  ( 0.000000000000000000, 0.000000000000000000, 1.000000000000000000 ) ) ;
#19046=VECTOR ( 'NONE', #2402, 1000.000000000000000 ) ;
#19047=EDGE_CURVE ( 'NONE', #2378, #8445, #1637, .T. ) ;
#19067=DIRECTION ( 'NONE',  ( 0.000000000000000000, -0.000000000000000000, -1.000000000000000000 ) ) ;
#19074=ORIENTED_EDGE ( 'NONE', *, *, #23165, .F. ) ;
#19075=AXIS2_PLACEMENT_3D ( 'NONE', #19299, #4180, #13434 ) ;
#19083=DIRECTION ( 'NONE',  ( -0.000000000000000000, -0.000000000000000000, -1.000000000000000000 ) ) ;
#19107=DIRECTION ( 'NONE',  ( 0.000000000000000000, 0.000000000000000000, 1.000000000000000000 ) ) ;
#19123=CARTESIAN_POINT ( 'NONE',  ( 42.00000000000000000, 0.000000000000000000, 0.000000000000000000 ) ) ;
#19125=ADVANCED_FACE ( 'NONE', ( #17668 ), #4752, .T. ) ;
#19130=CYLINDRICAL_SURFACE ( 'NONE', #24047, 1.000000000000000000 ) ;
#19136=CARTESIAN_POINT ( 'NONE',  ( -41.00000000000000000, -4.000000000000000888, 9.500000000000000000 ) ) ;
#19144=EDGE_CURVE ( 'NONE', #18828, #11172, #19942, .T. ) ;
#19153=VERTEX_POINT ( 'NONE', #21932 ) ;
#19154=EDGE_CURVE ( 'NONE', #3126, #11854, #1677, .T. ) ;
#19163=CYLINDRICAL_SURFACE ( 'NONE', #5957, 8.000000000000003553 ) ;
#19192=AXIS2_PLACEMENT_3D ( 'NONE', #6583, #8620, #3042 ) ;
#19193=AXIS2_PLACEMENT_3D ( 'NONE', #5019, #18061, #1358 ) ;
#19208=FACE_OUTER_BOUND ( 'NONE', #1546, .T. ) ;
#19209=VERTEX_POINT ( 'NONE', #18516 ) ;
#19219=ORIENTED_EDGE ( 'NONE', *, *, #9747, .T. ) ;
#19234=VECTOR ( 'NONE', #2945, 1000.000000000000000 ) ;
#19243=ADVANCED_FACE ( 'NONE', ( #14724 ), #1562, .T. ) ;
#19247=SHAPE_REPRESENTATION ( 'End Plate', ( #8005 ), #9178 ) ;
#19250=EDGE_CURVE ( 'NONE', #4159, #3260, #486, .T. ) ;
#19264=CARTESIAN_POINT ( 'NONE',  ( -29.00000000000000000, -29.49999999999999645, 11.00000000000000000 ) ) ;
#19265=DIRECTION ( 'NONE',  ( 1.000000000000000000, -2.600433232233976523E-16, 0.000000000000000000 ) ) ;
#19269=CARTESIAN_POINT ( 'NONE',  ( 41.00000000000000000, -6.000000000000015099, 11.00000000000000000 ) ) ;
#19284=CARTESIAN_POINT ( 'NONE',  ( 42.00000000000000000, 0.000000000000000000, 11.00000000000000000 ) ) ;
#19287=DIRECTION ( 'NONE',  ( -0.000000000000000000, -0.000000000000000000, -1.000000000000000000 ) ) ;
#19289=AXIS2_PLACEMENT_3D ( 'NONE', #13957, #1035, #23365 ) ;
#19291=ORIENTED_EDGE ( 'NONE', *, *, #23660, .F. ) ;
#19299=CARTESIAN_POINT ( 'NONE',  ( -34.00000000000000000, -3.999999999999999112, 10.49999999999999822 ) ) ;
#19309=ORIENTED_EDGE ( 'NONE', *, *, #13151, .F. ) ;
#19319=VERTEX_POINT ( 'NONE', #23663 ) ;
#19322=CIRCLE ( 'NONE', #2600, 19.84999999999999787 ) ;
#19325=VERTEX_POINT ( 'NONE', #4233 ) ;
#19326=DIRECTION ( 'NONE',  ( -0.000000000000000000, -0.000000000000000000, 1.000000000000000000 ) ) ;
#19337=DIRECTION ( 'NONE',  ( -0.000000000000000000, 0.000000000000000000, 1.000000000000000000 ) ) ;
#19343=DIRECTION ( 'NONE',  ( 0.000000000000000000, 1.000000000000000000, 0.000000000000000000 ) ) ;
#19348=ORIENTED_EDGE ( 'NONE', *, *, #17397, .T. ) ;
#19350=EDGE_LOOP ( 'NONE', ( #6161, #7250, #22545, #7888 ) ) ;
#19351=EDGE_LOOP ( 'NONE', ( #19309, #18620, #20915 ) ) ;
#19375=AXIS2_PLACEMENT_3D ( 'NONE', #14900, #22719, #22372 ) ;
#19376=DIRECTION ( 'NONE',  ( 1.000000000000000000, -6.938893903907222067E-15, 0.000000000000000000 ) ) ;
#19377=ORIENTED_EDGE ( 'NONE', *, *, #10211, .F. ) ;
#19378=VERTEX_POINT ( 'NONE', #16907 ) ;
#19383=DIRECTION ( 'NONE',  ( -1.000000000000000000, 0.000000000000000000, 0.000000000000000000 ) ) ;
#19390=FACE_OUTER_BOUND ( 'NONE', #8829, .T. ) ;
#19394=EDGE_CURVE ( 'NONE', #21975, #20352, #21533, .T. ) ;
#19396=DIRECTION ( 'NONE',  ( -0.000000000000000000, -0.000000000000000000, -1.000000000000000000 ) ) ;
#19398=ORIENTED_EDGE ( 'NONE', *, *, #23341, .F. ) ;
#19413=EDGE_CURVE ( 'NONE', #9925, #8713, #9039, .T. ) ;
#19416=EDGE_LOOP ( 'NONE', ( #4498, #23229, #10938 ) ) ;
#19418=FACE_OUTER_BOUND ( 'NONE', #13526, .T. ) ;
#19420=VECTOR ( 'NONE', #20455, 1000.000000000000000 ) ;
#19426=LINE ( 'NONE', #21116, #23214 ) ;
#19435=CIRCLE ( 'NONE', #10453, 2.500000000000002220 ) ;
#19436=VERTEX_POINT ( 'NONE', #15177 ) ;
#19459=EDGE_CURVE ( 'NONE', #1636, #19800, #17917, .T. ) ;
#19466=DIRECTION ( 'NONE',  ( -1.000000000000000000, 0.000000000000000000, 0.000000000000000000 ) ) ;
#19475=CARTESIAN_POINT ( 'NONE',  ( 1.999999999999994449, -45.00000000000000000, 3.000000000000002665 ) ) ;
#19479=ORIENTED_EDGE ( 'NONE', *, *, #3345, .F. ) ;
#19489=VERTEX_POINT ( 'NONE', #21431 ) ;
#19496=FACE_OUTER_BOUND ( 'NONE', #11309, .T. ) ;
#19504=DIRECTION ( 'NONE',  ( -0.000000000000000000, 0.000000000000000000, 1.000000000000000000 ) ) ;
#19514=ORIENTED_EDGE ( 'NONE', *, *, #8822, .T. ) ;
#19515=AXIS2_PLACEMENT_3D ( 'NONE', #11593, #6500, #17209 ) ;
#19522=LINE ( 'NONE', #23192, #14260 ) ;
#19523=CARTESIAN_POINT ( 'NONE',  ( 2.454813078130514813E-15, -16.67999999999999972, 13.00000000000000178 ) ) ;
#19526=CARTESIAN_POINT ( 'NONE',  ( 42.00000000000000000, 0.000000000000000000, 12.00000000000000000 ) ) ;
#19530=AXIS2_PLACEMENT_3D ( 'NONE', #16683, #22077, #9236 ) ;
#19535=CIRCLE ( 'NONE', #14841, 1.000000000000000888 ) ;
#19538=DIRECTION ( 'NONE',  ( -1.000000000000000000, 2.600433232233976523E-16, 0.000000000000000000 ) ) ;
#19549=CARTESIAN_POINT ( 'NONE',  ( -23.90000000000000568, 29.49999999999999645, 12.00000000000000000 ) ) ;
#19553=CARTESIAN_POINT ( 'NONE',  ( 31.10231664966676846, -45.36128193761570770, 12.00000000000000000 ) ) ;
#19586=VECTOR ( 'NONE', #13990, 1000.000000000000000 ) ;
#19587=ORIENTED_EDGE ( 'NONE', *, *, #2089, .T. ) ;
#19591=AXIS2_PLACEMENT_3D ( 'NONE', #904, #2981, #781 ) ;
#19595=CARTESIAN_POINT ( 'NONE',  ( 29.00000000000000000, 29.50000000000000355, 12.00000000000000000 ) ) ;
#19600=EDGE_CURVE ( 'NONE', #5846, #7241, #13987, .T. ) ;
#19608=EDGE_CURVE ( 'NONE', #19153, #21270, #3236, .T. ) ;
#19610=TOROIDAL_SURFACE ( 'NONE', #14511, 2.500000000000001776, 1.000000000000000000 ) ;
#19620=AXIS2_PLACEMENT_3D ( 'NONE', #3907, #4034, #16480 ) ;
#19621=ORIENTED_EDGE ( 'NONE', *, *, #443, .T. ) ;
#19636=ADVANCED_FACE ( 'NONE', ( #7254 ), #18355, .F. ) ;
#19637=TOROIDAL_SURFACE ( 'NONE', #17274, 19.84999999999999787, 1.000000000000000000 ) ;
#19663=DIRECTION ( 'NONE',  ( 1.000000000000000000, 0.000000000000000000, -0.000000000000000000 ) ) ;
#19667=ORIENTED_EDGE ( 'NONE', *, *, #19834, .T. ) ;
#19673=LINE ( 'NONE', #23448, #23740 ) ;
#19675=CIRCLE ( 'NONE', #15346, 8.000000000000003553 ) ;
#19681=CARTESIAN_POINT ( 'NONE',  ( 41.00000000000000000, -26.23076770084981391, 12.00000000000000000 ) ) ;
#19694=ORIENTED_EDGE ( 'NONE', *, *, #320, .F. ) ;
#19704=ADVANCED_FACE ( 'NONE', ( #23503, #22156 ), #21899, .T. ) ;
#19721=DIRECTION ( 'NONE',  ( -0.000000000000000000, 0.000000000000000000, 1.000000000000000000 ) ) ;
#19722=ORIENTED_EDGE ( 'NONE', *, *, #4700, .F. ) ;
#19726=CARTESIAN_POINT ( 'NONE',  ( -28.00000000000000355, -3.851859888774471706E-31, 12.00000000000000000 ) ) ;
#19735=FACE_OUTER_BOUND ( 'NONE', #23144, .T. ) ;
#19738=DIRECTION ( 'NONE',  ( 1.000000000000000000, 0.000000000000000000, 0.000000000000000000 ) ) ;
#19739=DIRECTION ( 'NONE',  ( 0.000000000000000000, -0.000000000000000000, -1.000000000000000000 ) ) ;
#19745=ORIENTED_EDGE ( 'NONE', *, *, #9758, .T. ) ;
#19749=AXIS2_PLACEMENT_3D ( 'NONE', #5062, #10529, #17989 ) ;
#19750=VERTEX_POINT ( 'NONE', #23846 ) ;
#19751=ORIENTED_EDGE ( 'NONE', *, *, #8473, .F. ) ;
#19752=CARTESIAN_POINT ( 'NONE',  ( -29.00000000000000000, -29.49999999999999645, 0.000000000000000000 ) ) ;
#19754=ADVANCED_FACE ( 'NONE', ( #7128 ), #2318, .F. ) ;
#19765=ORIENTED_EDGE ( 'NONE', *, *, #21700, .F. ) ;
#19783=EDGE_CURVE ( 'NONE', #4241, #10216, #2215, .T. ) ;
#19785=CARTESIAN_POINT ( 'NONE',  ( 20.99999999999999645, -29.50000000000000355, 11.50000000000000000 ) ) ;
#19787=ADVANCED_FACE ( 'NONE', ( #3585 ), #9638, .F. ) ;
#19793=DIRECTION ( 'NONE',  ( 0.000000000000000000, 0.000000000000000000, 1.000000000000000000 ) ) ;
#19794=DIRECTION ( 'NONE',  ( -0.4828336235133057208, -0.8757121056631633760, 0.000000000000000000 ) ) ;
#19796=CYLINDRICAL_SURFACE ( 'NONE', #10069, 1.000000000000000000 ) ;
#19798=ORIENTED_EDGE ( 'NONE', *, *, #9030, .F. ) ;
#19800=VERTEX_POINT ( 'NONE', #280 ) ;
#19801=CARTESIAN_POINT ( 'NONE',  ( 33.99999999999998579, -1.387778780781445676E-14, 9.500000000000000000 ) ) ;
#19815=ORIENTED_EDGE ( 'NONE', *, *, #12004, .F. ) ;
#19817=CARTESIAN_POINT ( 'NONE',  ( -20.64923905428957340, -37.45138642374540439, 12.00000000000000000 ) ) ;
#19818=ORIENTED_EDGE ( 'NONE', *, *, #17445, .T. ) ;
#19826=CARTESIAN_POINT ( 'NONE',  ( -28.27483331787888332, -41.23752903419610050, 0.000000000000000000 ) ) ;
#19834=EDGE_CURVE ( 'NONE', #758, #9485, #12050, .T. ) ;
#19837=DIRECTION ( 'NONE',  ( 1.000000000000000000, 0.000000000000000000, 0.000000000000000000 ) ) ;
#19860=ADVANCED_FACE ( 'NONE', ( #17084 ), #7794, .T. ) ;
#19871=CARTESIAN_POINT ( 'NONE',  ( 33.99999999999998579, -1.387778780781445676E-14, 11.00000000000000000 ) ) ;
#19875=CYLINDRICAL_SURFACE ( 'NONE', #900, 1.000000000000000000 ) ;
#19877=ADVANCED_FACE ( 'NONE', ( #11830 ), #17455, .T. ) ;
#19881=EDGE_CURVE ( 'NONE', #2518, #7729, #15, .T. ) ;
#19893=ORIENTED_EDGE ( 'NONE', *, *, #21367, .F. ) ;
#19894=ORIENTED_EDGE ( 'NONE', *, *, #1914, .F. ) ;
#19911=ORIENTED_EDGE ( 'NONE', *, *, #23165, .T. ) ;
#19924=EDGE_CURVE ( 'NONE', #9530, #16881, #15972, .T. ) ;
#19931=CARTESIAN_POINT ( 'NONE',  ( 40.77574956473004164, -27.49633847812775755, 12.00000000000000000 ) ) ;
#19935=VECTOR ( 'NONE', #10915, 1000.000000000000000 ) ;
#19936=CARTESIAN_POINT ( 'NONE',  ( -39.00000000000000000, 28.80990663662251450, 12.00000000000000000 ) ) ;
#19937=VERTEX_POINT ( 'NONE', #1368 ) ;
#19942=CIRCLE ( 'NONE', #23058, 4.999999999999997335 ) ;
#19946=CIRCLE ( 'NONE', #9789, 1.999999999999994449 ) ;
#19949=VERTEX_POINT ( 'NONE', #23209 ) ;
#19957=CARTESIAN_POINT ( 'NONE',  ( -34.00000000000000000, -3.851859888774471706E-31, 12.00000000000000000 ) ) ;
#19982=EDGE_CURVE ( 'NONE', #11172, #21057, #23072, .T. ) ;
#19986=AXIS2_PLACEMENT_3D ( 'NONE', #8477, #15198, #2870 ) ;
#19994=EDGE_CURVE ( 'NONE', #21048, #14261, #1124, .T. ) ;
#20008=DIRECTION ( 'NONE',  ( 0.000000000000000000, 1.000000000000000000, -0.000000000000000000 ) ) ;
#20009=AXIS2_PLACEMENT_3D ( 'NONE', #4841, #12372, #8712 ) ;
#20013=CARTESIAN_POINT ( 'NONE',  ( 33.99999999999998579, -1.387778780781445676E-14, 10.49999999999999822 ) ) ;
#20015=AXIS2_PLACEMENT_3D ( 'NONE', #23196, #11685, #741 ) ;
#20017=EDGE_CURVE ( 'NONE', #8481, #21886, #3068, .T. ) ;
#20019=CARTESIAN_POINT ( 'NONE',  ( -34.00000000000000000, -4.999999999999999112, 11.00000000000000000 ) ) ;
#20024=VECTOR ( 'NONE', #2244, 1000.000000000000000 ) ;
#20030=ORIENTED_EDGE ( 'NONE', *, *, #23123, .F. ) ;
#20033=CIRCLE ( 'NONE', #9473, 1.000000000000000000 ) ;
#20045=ORIENTED_EDGE ( 'NONE', *, *, #8444, .F. ) ;
#20049=DIRECTION ( 'NONE',  ( 1.000000000000000000, 0.000000000000000000, 0.000000000000000000 ) ) ;
#20062=( GEOMETRIC_REPRESENTATION_CONTEXT ( 3 ) GLOBAL_UNCERTAINTY_ASSIGNED_CONTEXT ( ( #15194 ) ) GLOBAL_UNIT_ASSIGNED_CONTEXT ( ( #10487, #10600, #6356 ) ) REPRESENTATION_CONTEXT ( 'NONE', 'WORKASPACE' ) );
#20073=CARTESIAN_POINT ( 'NONE',  ( 0.000000000000000000, 0.000000000000000000, 11.00000000000000000 ) ) ;
#20075=EDGE_CURVE ( 'NONE', #17414, #2739, #3522, .T. ) ;
#20099=EDGE_LOOP ( 'NONE', ( #6239, #5883, #19798, #18064 ) ) ;
#20116=DIRECTION ( 'NONE',  ( 0.4828336235133057208, -0.8757121056631633760, 0.000000000000000000 ) ) ;
#20124=EDGE_LOOP ( 'NONE', ( #11030, #5033, #12824, #1594, #5684, #1673, #20500, #3963, #20144, #5873 ) ) ;
#20125=TOROIDAL_SURFACE ( 'NONE', #10742, 21.85000000000000142, 1.000000000000000000 ) ;
#20139=CARTESIAN_POINT ( 'NONE',  ( 27.70933665152130132, 40.41277845351218190, 12.00000000000000000 ) ) ;
#20144=ORIENTED_EDGE ( 'NONE', *, *, #19881, .F. ) ;
#20146=VERTEX_POINT ( 'NONE', #14639 ) ;
#20147=FACE_OUTER_BOUND ( 'NONE', #15036, .T. ) ;
#20149=CARTESIAN_POINT ( 'NONE',  ( 42.00000000000000000, -5.000000000000016875, 8.500000000000000000 ) ) ;
#20152=DIRECTION ( 'NONE',  ( -0.8757121056631640421, 0.4828336235133042775, 0.000000000000000000 ) ) ;
#20154=DIRECTION ( 'NONE',  ( 1.000000000000000000, 0.000000000000000000, 0.000000000000000000 ) ) ;
#20156=DIRECTION ( 'NONE',  ( 0.8757121056631640421, -0.4828336235133042775, 0.000000000000000000 ) ) ;
#20159=VECTOR ( 'NONE', #20380, 1000.000000000000000 ) ;
#20171=CARTESIAN_POINT ( 'NONE',  ( -34.00000000000000000, 4.999999999999999112, 9.500000000000000000 ) ) ;
#20182=EDGE_CURVE ( 'NONE', #1507, #9181, #22605, .T. ) ;
#20199=CARTESIAN_POINT ( 'NONE',  ( -40.77574956473004164, 27.49633847812775755, 11.00000000000000000 ) ) ;
#20206=CYLINDRICAL_SURFACE ( 'NONE', #23510, 4.999999999999997335 ) ;
#20218=ORIENTED_EDGE ( 'NONE', *, *, #20814, .T. ) ;
#20237=ORIENTED_EDGE ( 'NONE', *, *, #2738, .F. ) ;
#20251=ORIENTED_EDGE ( 'NONE', *, *, #2815, .T. ) ;
#20254=ORIENTED_EDGE ( 'NONE', *, *, #2880, .T. ) ;
#20257=DIRECTION ( 'NONE',  ( 0.000000000000000000, -1.000000000000000000, 0.000000000000000000 ) ) ;
#20272=DIRECTION ( 'NONE',  ( -0.000000000000000000, -0.000000000000000000, 1.000000000000000000 ) ) ;
#20282=EDGE_CURVE ( 'NONE', #4922, #7241, #20614, .T. ) ;
#20292=CIRCLE ( 'NONE', #808, 1.500000000000001332 ) ;
#20295=ORIENTED_EDGE ( 'NONE', *, *, #14086, .F. ) ;
#20298=CARTESIAN_POINT ( 'NONE',  ( 33.99999999999998579, 5.999999999999985789, 12.00000000000000000 ) ) ;
#20303=ORIENTED_EDGE ( 'NONE', *, *, #10998, .T. ) ;
#20315=LINE ( 'NONE', #16752, #6081 ) ;
#20327=ORIENTED_EDGE ( 'NONE', *, *, #20584, .F. ) ;
#20330=CARTESIAN_POINT ( 'NONE',  ( -20.99999999999999645, 29.49999999999999645, 11.50000000000000000 ) ) ;
#20338=CARTESIAN_POINT ( 'NONE',  ( 20.64923905428957340, 37.45138642374540439, 12.00000000000000000 ) ) ;
#20348=ORIENTED_EDGE ( 'NONE', *, *, #3511, .F. ) ;
#20352=VERTEX_POINT ( 'NONE', #15850 ) ;
#20360=CIRCLE ( 'NONE', #6340, 1.000000000000000888 ) ;
#20363=VERTEX_POINT ( 'NONE', #15713 ) ;
#20364=AXIS2_PLACEMENT_3D ( 'NONE', #18338, #16625, #24064 ) ;
#20380=DIRECTION ( 'NONE',  ( 0.000000000000000000, 1.000000000000000000, -0.000000000000000000 ) ) ;
#20387=EDGE_LOOP ( 'NONE', ( #12464, #8319 ) ) ;
#20397=EDGE_LOOP ( 'NONE', ( #8105, #18762, #14516, #2700 ) ) ;
#20426=DIRECTION ( 'NONE',  ( -1.000000000000000000, 0.000000000000000000, 0.000000000000000000 ) ) ;
#20430=DIRECTION ( 'NONE',  ( -0.9913301211009815095, -0.1313947906041688374, 0.000000000000000000 ) ) ;
#20434=CIRCLE ( 'NONE', #20833, 1.000000000000000888 ) ;
#20442=EDGE_LOOP ( 'NONE', ( #3799, #10500, #16484, #17371, #1292 ) ) ;
#20455=DIRECTION ( 'NONE',  ( -0.000000000000000000, -0.000000000000000000, -1.000000000000000000 ) ) ;
#20456=CARTESIAN_POINT ( 'NONE',  ( 20.99999999999999645, -29.50000000000000355, 12.00000000000000000 ) ) ;
#20469=LINE ( 'NONE', #11648, #3700 ) ;
#20471=DIRECTION ( 'NONE',  ( -0.000000000000000000, -0.000000000000000000, 1.000000000000000000 ) ) ;
#20475=ORIENTED_EDGE ( 'NONE', *, *, #14447, .F. ) ;
#20480=EDGE_LOOP ( 'NONE', ( #8503, #22442, #23231, #663 ) ) ;
#20484=EDGE_CURVE ( 'NONE', #20529, #18828, #9885, .T. ) ;
#20486=CARTESIAN_POINT ( 'NONE',  ( -39.00000000000000000, -28.80990663662251805, 12.00000000000000000 ) ) ;
#20489=VERTEX_POINT ( 'NONE', #17808 ) ;
#20493=CARTESIAN_POINT ( 'NONE',  ( -42.00000000000000000, -26.82133436441678853, 11.00000000000000000 ) ) ;
#20500=ORIENTED_EDGE ( 'NONE', *, *, #18054, .T. ) ;
#20503=CARTESIAN_POINT ( 'NONE',  ( 31.10231664966676846, 45.36128193761570770, 12.00000000000000000 ) ) ;
#20507=DIRECTION ( 'NONE',  ( 0.000000000000000000, -6.938893903907222067E-15, 1.000000000000000000 ) ) ;
#20514=CARTESIAN_POINT ( 'NONE',  ( -29.00000000000000000, 29.49999999999999645, 0.000000000000000000 ) ) ;
#20516=CARTESIAN_POINT ( 'NONE',  ( -34.00000000000000000, -3.851859888774471706E-31, 9.500000000000000000 ) ) ;
#20529=VERTEX_POINT ( 'NONE', #9233 ) ;
#20534=DIRECTION ( 'NONE',  ( -0.1313947906041722513, -0.9913301211009810654, 0.000000000000000000 ) ) ;
#20539=ORIENTED_EDGE ( 'NONE', *, *, #6715, .F. ) ;
#20543=CARTESIAN_POINT ( 'NONE',  ( 39.00000000000000000, 29.49999999999999645, 12.00000000000000000 ) ) ;
#20551=DIRECTION ( 'NONE',  ( -0.000000000000000000, 0.000000000000000000, 1.000000000000000000 ) ) ;
#20552=DIRECTION ( 'NONE',  ( 1.000000000000000000, 0.000000000000000000, 0.000000000000000000 ) ) ;
#20562=DIRECTION ( 'NONE',  ( 0.000000000000000000, 0.000000000000000000, 1.000000000000000000 ) ) ;
#20564=DIRECTION ( 'NONE',  ( 0.000000000000000000, -1.000000000000000000, 0.000000000000000000 ) ) ;
#20572=ORIENTED_EDGE ( 'NONE', *, *, #2684, .T. ) ;
#20579=CARTESIAN_POINT ( 'NONE',  ( -21.13207267780287069, -38.32709852940855910, 0.000000000000000000 ) ) ;
#20584=EDGE_CURVE ( 'NONE', #11167, #8265, #5100, .T. ) ;
#20597=EDGE_CURVE ( 'NONE', #11492, #11172, #22004, .T. ) ;
#20604=CARTESIAN_POINT ( 'NONE',  ( 27.70933665152130843, -40.41277845351217479, 12.00000000000000000 ) ) ;
#20607=LINE ( 'NONE', #2045, #21935 ) ;
#20610=EDGE_CURVE ( 'NONE', #8445, #19153, #9900, .T. ) ;
#20614=LINE ( 'NONE', #3893, #17300 ) ;
#20616=VERTEX_POINT ( 'NONE', #7040 ) ;
#20618=EDGE_LOOP ( 'NONE', ( #21787, #9780, #18670, #6352 ) ) ;
#20623=CARTESIAN_POINT ( 'NONE',  ( 34.10000000000000142, 29.50000000000000355, 0.000000000000000000 ) ) ;
#20624=CARTESIAN_POINT ( 'NONE',  ( -40.00000000000000000, 0.000000000000000000, 12.00000000000000000 ) ) ;
#20630=CARTESIAN_POINT ( 'NONE',  ( -20.84999999999999787, 16.67999999999985405, 13.50000000000000178 ) ) ;
#20646=FACE_OUTER_BOUND ( 'NONE', #13197, .T. ) ;
#20650=VECTOR ( 'NONE', #17950, 1000.000000000000000 ) ;
#20653=CARTESIAN_POINT ( 'NONE',  ( 2.454813078130514813E-15, -16.67999999999999972, 14.50000000000000000 ) ) ;
#20659=CARTESIAN_POINT ( 'NONE',  ( 29.00000000000000000, -29.50000000000000355, 0.000000000000000000 ) ) ;
#20668=CARTESIAN_POINT ( 'NONE',  ( 21.85000000000000497, -16.67999999999999616, 12.00000000000000000 ) ) ;
#20677=ORIENTED_EDGE ( 'NONE', *, *, #14008, .T. ) ;
#20686=CARTESIAN_POINT ( 'NONE',  ( 41.00000000000000000, 4.999999999999986677, 10.49999999999999822 ) ) ;
#20688=CARTESIAN_POINT ( 'NONE',  ( 37.00000000000000711, 29.50000000000000355, 11.50000000000000000 ) ) ;
#20689=DIRECTION ( 'NONE',  ( -0.000000000000000000, -0.000000000000000000, 1.000000000000000000 ) ) ;
#20694=DIRECTION ( 'NONE',  ( 0.000000000000000000, -1.000000000000000000, 0.000000000000000000 ) ) ;
#20699=CARTESIAN_POINT ( 'NONE',  ( 39.00000000000000000, -28.80990663662251805, 11.00000000000000000 ) ) ;
#20700=DIRECTION ( 'NONE',  ( -0.000000000000000000, 0.000000000000000000, 1.000000000000000000 ) ) ;
#20708=( LENGTH_UNIT ( ) NAMED_UNIT ( * ) SI_UNIT ( .MILLI., .METRE. ) );
#20719=ORIENTED_EDGE ( 'NONE', *, *, #6715, .T. ) ;
#20738=DIRECTION ( 'NONE',  ( 1.000000000000000000, 0.000000000000000000, 0.000000000000000000 ) ) ;
#20742=AXIS2_PLACEMENT_3D ( 'NONE', #16100, #21364, #6714 ) ;
#20746=EDGE_CURVE ( 'NONE', #9207, #18239, #1739, .T. ) ;
#20776=EDGE_CURVE ( 'NONE', #10733, #22129, #14196, .T. ) ;
#20781=CIRCLE ( 'NONE', #2863, 4.999999999999997335 ) ;
#20795=ORIENTED_EDGE ( 'NONE', *, *, #7427, .T. ) ;
#20796=CIRCLE ( 'NONE', #14550, 1.000000000000000888 ) ;
#20800=CIRCLE ( 'NONE', #16509, 8.000000000000003553 ) ;
#20812=EDGE_LOOP ( 'NONE', ( #6246, #13936, #15450, #23619 ) ) ;
#20814=EDGE_CURVE ( 'NONE', #1231, #13221, #10203, .T. ) ;
#20820=ORIENTED_EDGE ( 'NONE', *, *, #22889, .T. ) ;
#20821=FACE_OUTER_BOUND ( 'NONE', #1264, .T. ) ;
#20833=AXIS2_PLACEMENT_3D ( 'NONE', #11606, #1984, #2114 ) ;
#20838=DIRECTION ( 'NONE',  ( 1.000000000000000000, 0.000000000000000000, 0.000000000000000000 ) ) ;
#20841=EDGE_CURVE ( 'NONE', #16095, #22169, #16897, .T. ) ;
#20853=AXIS2_PLACEMENT_3D ( 'NONE', #9677, #21384, #23225 ) ;
#20859=VECTOR ( 'NONE', #4372, 1000.000000000000000 ) ;
#20860=LINE ( 'NONE', #21078, #9402 ) ;
#20868=ORIENTED_EDGE ( 'NONE', *, *, #20746, .T. ) ;
#20873=EDGE_LOOP ( 'NONE', ( #17411, #7971, #5454, #4526 ) ) ;
#20890=AXIS2_PLACEMENT_3D ( 'NONE', #5905, #2250, #9417 ) ;
#20894=EDGE_CURVE ( 'NONE', #15347, #5011, #16927, .T. ) ;
#20897=CARTESIAN_POINT ( 'NONE',  ( -34.00000000000000000, 4.999999999999999112, 10.49999999999999822 ) ) ;
#20899=DIRECTION ( 'NONE',  ( -0.000000000000000000, 1.000000000000000000, -0.000000000000000000 ) ) ;
#20900=ADVANCED_FACE ( 'NONE', ( #12872 ), #8753, .F. ) ;
#20903=CARTESIAN_POINT ( 'NONE',  ( 41.00000000000000000, 3.999999999999987121, 10.49999999999999822 ) ) ;
#20915=ORIENTED_EDGE ( 'NONE', *, *, #15456, .T. ) ;
#20919=CARTESIAN_POINT ( 'NONE',  ( 0.000000000000000000, 0.000000000000000000, 0.000000000000000000 ) ) ;
#20923=LINE ( 'NONE', #4206, #16118 ) ;
#20924=ORIENTED_EDGE ( 'NONE', *, *, #768, .F. ) ;
#20926=ADVANCED_FACE ( 'NONE', ( #16771 ), #9127, .T. ) ;
#20936=AXIS2_PLACEMENT_3D ( 'NONE', #23813, #7088, #7874 ) ;
#20939=DIRECTION ( 'NONE',  ( 0.000000000000000000, -0.000000000000000000, -1.000000000000000000 ) ) ;
#20942=VERTEX_POINT ( 'NONE', #20456 ) ;
#20953=DIRECTION ( 'NONE',  ( 1.000000000000000000, 0.000000000000000000, -0.000000000000000000 ) ) ;
#20954=ADVANCED_FACE ( 'NONE', ( #11638 ), #2512, .T. ) ;
#20969=ORIENTED_EDGE ( 'NONE', *, *, #14447, .T. ) ;
#20970=DIRECTION ( 'NONE',  ( 0.8757121056631641531, 0.4828336235133042775, 0.000000000000000000 ) ) ;
#20978=ADVANCED_FACE ( 'NONE', ( #21176 ), #13729, .F. ) ;
#20981=AXIS2_PLACEMENT_3D ( 'NONE', #13065, #15231, #7682 ) ;
#20982=ORIENTED_EDGE ( 'NONE', *, *, #9758, .F. ) ;
#20986=ORIENTED_EDGE ( 'NONE', *, *, #10823, .T. ) ;
#20988=DIRECTION ( 'NONE',  ( 3.469446951953610639E-15, 1.000000000000000000, -0.000000000000000000 ) ) ;
#20991=LINE ( 'NONE', #2320, #22059 ) ;
#20995=ORIENTED_EDGE ( 'NONE', *, *, #17628, .F. ) ;
#20996=LINE ( 'NONE', #15367, #16465 ) ;
#21001=DIRECTION ( 'NONE',  ( -1.000000000000000000, 0.000000000000000000, 0.000000000000000000 ) ) ;
#21005=CARTESIAN_POINT ( 'NONE',  ( 41.00000000000000000, 0.000000000000000000, 12.00000000000000000 ) ) ;
#21006=DIRECTION ( 'NONE',  ( 1.000000000000000000, 0.000000000000000000, 0.000000000000000000 ) ) ;
#21010=DIRECTION ( 'NONE',  ( 1.000000000000000000, 0.000000000000000000, 0.000000000000000000 ) ) ;
#21026=EDGE_LOOP ( 'NONE', ( #7527, #6061, #1189 ) ) ;
#21029=ORIENTED_EDGE ( 'NONE', *, *, #5039, .F. ) ;
#21032=FACE_OUTER_BOUND ( 'NONE', #19416, .T. ) ;
#21034=ORIENTED_EDGE ( 'NONE', *, *, #9138, .T. ) ;
#21037=DIRECTION ( 'NONE',  ( -0.000000000000000000, -0.000000000000000000, -1.000000000000000000 ) ) ;
#21038=ORIENTED_EDGE ( 'NONE', *, *, #9315, .F. ) ;
#21048=VERTEX_POINT ( 'NONE', #14496 ) ;
#21050=DIRECTION ( 'NONE',  ( -0.000000000000000000, -0.000000000000000000, -1.000000000000000000 ) ) ;
#21053=ORIENTED_EDGE ( 'NONE', *, *, #18306, .T. ) ;
#21057=VERTEX_POINT ( 'NONE', #5370 ) ;
#21072=CARTESIAN_POINT ( 'NONE',  ( -29.00000000000000000, 29.49999999999999645, 12.00000000000000000 ) ) ;
#21073=ORIENTED_EDGE ( 'NONE', *, *, #8822, .F. ) ;
#21074=EDGE_CURVE ( 'NONE', #18986, #15347, #7308, .T. ) ;
#21078=CARTESIAN_POINT ( 'NONE',  ( 42.00000000000000000, -5.000000000000015099, 11.00000000000000000 ) ) ;
#21084=AXIS2_PLACEMENT_3D ( 'NONE', #6438, #13744, #19376 ) ;
#21087=CIRCLE ( 'NONE', #3170, 4.999999999999997335 ) ;
#21097=EDGE_CURVE ( 'NONE', #23250, #17123, #5277, .T. ) ;
#21100=FACE_OUTER_BOUND ( 'NONE', #419, .T. ) ;
#21102=EDGE_CURVE ( 'NONE', #10216, #16364, #4582, .T. ) ;
#21109=ORIENTED_EDGE ( 'NONE', *, *, #17396, .T. ) ;
#21116=CARTESIAN_POINT ( 'NONE',  ( 20.99999999999999645, 29.50000000000000355, 11.50000000000000000 ) ) ;
#21117=ORIENTED_EDGE ( 'NONE', *, *, #17150, .T. ) ;
#21130=CARTESIAN_POINT ( 'NONE',  ( 0.000000000000000000, 0.000000000000000000, 11.00000000000000000 ) ) ;
#21133=ORIENTED_EDGE ( 'NONE', *, *, #12996, .F. ) ;
#21142=VECTOR ( 'NONE', #23951, 1000.000000000000000 ) ;
#21147=FACE_BOUND ( 'NONE', #15256, .T. ) ;
#21148=DIRECTION ( 'NONE',  ( -0.8247505806839219300, 0.5654966663575777819, 0.000000000000000000 ) ) ;
#21149=DIRECTION ( 'NONE',  ( -0.000000000000000000, -1.000000000000000000, -0.000000000000000000 ) ) ;
#21166=ADVANCED_FACE ( 'NONE', ( #4377 ), #11666, .T. ) ;
#21172=ORIENTED_EDGE ( 'NONE', *, *, #24032, .T. ) ;
#21176=FACE_OUTER_BOUND ( 'NONE', #2477, .T. ) ;
#21178=ORIENTED_EDGE ( 'NONE', *, *, #12004, .T. ) ;
#21180=DIRECTION ( 'NONE',  ( 0.000000000000000000, 1.000000000000000000, 0.000000000000000000 ) ) ;
#21182=DIRECTION ( 'NONE',  ( 0.8757121056631641531, -0.4828336235133042775, 0.000000000000000000 ) ) ;
#21192=CIRCLE ( 'NONE', #21982, 8.000000000000003553 ) ;
#21197=VERTEX_POINT ( 'NONE', #246 ) ;
#21202=CARTESIAN_POINT ( 'NONE',  ( -34.10000000000000142, 29.49999999999999645, 0.000000000000000000 ) ) ;
#21208=CIRCLE ( 'NONE', #16136, 8.000000000000003553 ) ;
#21209=CIRCLE ( 'NONE', #3291, 8.000000000000003553 ) ;
#21211=FACE_OUTER_BOUND ( 'NONE', #7045, .T. ) ;
#21215=ORIENTED_EDGE ( 'NONE', *, *, #22673, .F. ) ;
#21216=CARTESIAN_POINT ( 'NONE',  ( 19.85000000000000142, 16.67999999999999972, 13.50000000000000178 ) ) ;
#21217=DIRECTION ( 'NONE',  ( 0.000000000000000000, -1.000000000000000000, 0.000000000000000000 ) ) ;
#21219=DIRECTION ( 'NONE',  ( 0.000000000000000000, 0.000000000000000000, -1.000000000000000000 ) ) ;
#21228=CARTESIAN_POINT ( 'NONE',  ( -40.29291594121673370, -26.62062637246459218, 12.00000000000000000 ) ) ;
#21229=ADVANCED_FACE ( 'NONE', ( #2258 ), #13483, .F. ) ;
#21249=CARTESIAN_POINT ( 'NONE',  ( -40.00000000000000000, 28.80990663662251450, 11.00000000000000000 ) ) ;
#21253=ORIENTED_EDGE ( 'NONE', *, *, #16998, .T. ) ;
#21260=VERTEX_POINT ( 'NONE', #8443 ) ;
#21270=VERTEX_POINT ( 'NONE', #15160 ) ;
#21272=CIRCLE ( 'NONE', #16589, 4.999999999999997335 ) ;
#21282=DIRECTION ( 'NONE',  ( 0.000000000000000000, 0.000000000000000000, 1.000000000000000000 ) ) ;
#21303=AXIS2_PLACEMENT_3D ( 'NONE', #5771, #11595, #38 ) ;
#21306=DIRECTION ( 'NONE',  ( 1.000000000000000000, 0.000000000000000000, 0.000000000000000000 ) ) ;
#21318=LINE ( 'NONE', #11645, #19586 ) ;
#21326=ORIENTED_EDGE ( 'NONE', *, *, #10998, .F. ) ;
#21339=ADVANCED_FACE ( 'NONE', ( #7837 ), #10503, .F. ) ;
#21340=CYLINDRICAL_SURFACE ( 'NONE', #196, 1.000000000000000000 ) ;
#21352=VERTEX_POINT ( 'NONE', #13944 ) ;
#21364=DIRECTION ( 'NONE',  ( -0.000000000000000000, -0.000000000000000000, -1.000000000000000000 ) ) ;
#21367=EDGE_CURVE ( 'NONE', #19378, #977, #593, .T. ) ;
#21370=DIRECTION ( 'NONE',  ( 1.000000000000000000, 0.000000000000000000, 0.000000000000000000 ) ) ;
#21376=DIRECTION ( 'NONE',  ( -0.000000000000000000, -0.000000000000000000, 1.000000000000000000 ) ) ;
#21384=DIRECTION ( 'NONE',  ( -0.000000000000000000, -0.000000000000000000, -1.000000000000000000 ) ) ;
#21395=EDGE_CURVE ( 'NONE', #19319, #23989, #23979, .T. ) ;
#21397=EDGE_CURVE ( 'NONE', #1596, #21725, #18438, .T. ) ;
#21398=DIRECTION ( 'NONE',  ( -0.000000000000000000, 0.000000000000000000, 1.000000000000000000 ) ) ;
#21404=FACE_OUTER_BOUND ( 'NONE', #17040, .T. ) ;
#21406=STYLED_ITEM('',(#24148),#2277);
#21408=ORIENTED_EDGE ( 'NONE', *, *, #13182, .T. ) ;
#21409=DIRECTION ( 'NONE',  ( 1.000000000000000000, 0.000000000000000000, -0.000000000000000000 ) ) ;
#21412=ORIENTED_EDGE ( 'NONE', *, *, #19413, .T. ) ;
#21414=ORIENTED_EDGE ( 'NONE', *, *, #5965, .T. ) ;
#21418=CARTESIAN_POINT ( 'NONE',  ( 28.99999999999998934, -1.387778780781445676E-14, 10.49999999999999822 ) ) ;
#21424=CARTESIAN_POINT ( 'NONE',  ( -19.84999999999999787, 16.67999999999999972, 13.50000000000000178 ) ) ;
#21431=CARTESIAN_POINT ( 'NONE',  ( 1.016919733032271456, 45.00000000000000000, 0.02500000000000418554 ) ) ;
#21439=EDGE_LOOP ( 'NONE', ( #23054, #10474, #10759, #6511 ) ) ;
#21446=EDGE_LOOP ( 'NONE', ( #20045, #19348, #11279, #366 ) ) ;
#21466=EDGE_LOOP ( 'NONE', ( #19751, #7160, #10817, #6332 ) ) ;
#21479=ADVANCED_FACE ( 'NONE', ( #5141 ), #14651, .F. ) ;
#21488=DIRECTION ( 'NONE',  ( 1.000000000000000000, 0.000000000000000000, 0.000000000000000000 ) ) ;
#21493=DIRECTION ( 'NONE',  ( -0.000000000000000000, 0.000000000000000000, 1.000000000000000000 ) ) ;
#21506=ORIENTED_EDGE ( 'NONE', *, *, #18556, .F. ) ;
#21512=VERTEX_POINT ( 'NONE', #3795 ) ;
#21515=AXIS2_PLACEMENT_3D ( 'NONE', #15488, #9738, #22955 ) ;
#21518=DIRECTION ( 'NONE',  ( -1.000000000000000000, -0.000000000000000000, -0.000000000000000000 ) ) ;
#21522=DIRECTION ( 'NONE',  ( 0.000000000000000000, -1.000000000000000000, 0.000000000000000000 ) ) ;
#21530=EDGE_CURVE ( 'NONE', #6705, #10396, #7548, .T. ) ;
#21533=CIRCLE ( 'NONE', #18781, 1.000000000000000888 ) ;
#21536=AXIS2_PLACEMENT_3D ( 'NONE', #5117, #14036, #10721 ) ;
#21541=AXIS2_PLACEMENT_3D ( 'NONE', #907, #9770, #10023 ) ;
#21542=DIRECTION ( 'NONE',  ( -0.000000000000000000, -0.000000000000000000, -1.000000000000000000 ) ) ;
#21543=CARTESIAN_POINT ( 'NONE',  ( -1.029124893018731811E-15, -45.00000000000000000, 4.201721238055123209 ) ) ;
#21546=ORIENTED_EDGE ( 'NONE', *, *, #15057, .F. ) ;
#21547=DIRECTION ( 'NONE',  ( 1.000000000000000000, 0.000000000000000000, 0.000000000000000000 ) ) ;
#21553=ADVANCED_FACE ( 'NONE', ( #14870 ), #5857, .T. ) ;
#21555=DIRECTION ( 'NONE',  ( -0.000000000000000000, -0.000000000000000000, -1.000000000000000000 ) ) ;
#21556=CIRCLE ( 'NONE', #17249, 1.000000000000000888 ) ;
#21557=AXIS2_PLACEMENT_3D ( 'NONE', #326, #7738, #22770 ) ;
#21560=EDGE_CURVE ( 'NONE', #19949, #977, #20991, .T. ) ;
#21567=EDGE_CURVE ( 'NONE', #12416, #3226, #14996, .T. ) ;
#21568=EDGE_CURVE ( 'NONE', #9530, #15114, #18676, .T. ) ;
#21573=ORIENTED_EDGE ( 'NONE', *, *, #23483, .F. ) ;
#21575=CARTESIAN_POINT ( 'NONE',  ( 0.000000000000000000, -45.00000000000000000, 0.000000000000000000 ) ) ;
#21581=TOROIDAL_SURFACE ( 'NONE', #9024, 10.00000000000000533, 1.000000000000000000 ) ;
#21583=AXIS2_PLACEMENT_3D ( 'NONE', #11275, #7507, #13378 ) ;
#21587=LINE ( 'NONE', #8133, #9023 ) ;
#21603=VECTOR ( 'NONE', #21542, 1000.000000000000000 ) ;
#21613=DIRECTION ( 'NONE',  ( 1.000000000000000000, 0.000000000000000000, 0.000000000000000000 ) ) ;
#21615=DIRECTION ( 'NONE',  ( 0.000000000000000000, 0.000000000000000000, -1.000000000000000000 ) ) ;
#21616=AXIS2_PLACEMENT_3D ( 'NONE', #12064, #1000, #23336 ) ;
#21621=FACE_OUTER_BOUND ( 'NONE', #19350, .T. ) ;
#21628=CARTESIAN_POINT ( 'NONE',  ( 40.00000000000000000, -28.80990663662251450, 12.00000000000000000 ) ) ;
#21629=DIRECTION ( 'NONE',  ( -1.000000000000000000, 0.000000000000000000, 0.000000000000000000 ) ) ;
#21636=ORIENTED_EDGE ( 'NONE', *, *, #3030, .F. ) ;
#21646=DIRECTION ( 'NONE',  ( 0.000000000000000000, 0.000000000000000000, 1.000000000000000000 ) ) ;
#21653=EDGE_CURVE ( 'NONE', #15898, #23250, #3906, .T. ) ;
#21656=CIRCLE ( 'NONE', #10391, 50.00000000000000000 ) ;
#21664=CARTESIAN_POINT ( 'NONE',  ( 2.454813078130514813E-15, 16.67999999999999972, 14.50000000000000000 ) ) ;
#21666=DIRECTION ( 'NONE',  ( 0.000000000000000000, 0.000000000000000000, 1.000000000000000000 ) ) ;
#21667=ORIENTED_EDGE ( 'NONE', *, *, #16587, .F. ) ;
#21679=CYLINDRICAL_SURFACE ( 'NONE', #7065, 20.85000000000000142 ) ;
#21687=TOROIDAL_SURFACE ( 'NONE', #1811, 5.999999999999999112, 1.000000000000000000 ) ;
#21691=EDGE_LOOP ( 'NONE', ( #6575, #2503, #3402, #819 ) ) ;
#21700=EDGE_CURVE ( 'NONE', #14909, #13595, #15594, .T. ) ;
#21705=EDGE_LOOP ( 'NONE', ( #2716, #848, #5357, #18586 ) ) ;
#21708=ORIENTED_EDGE ( 'NONE', *, *, #1559, .F. ) ;
#21725=VERTEX_POINT ( 'NONE', #851 ) ;
#21728=FACE_OUTER_BOUND ( 'NONE', #20618, .T. ) ;
#21730=PLANE ( 'NONE',  #21536 ) ;
#21746=EDGE_LOOP ( 'NONE', ( #3698, #20303, #9344, #23372 ) ) ;
#21754=FACE_OUTER_BOUND ( 'NONE', #16058, .T. ) ;
#21758=ORIENTED_EDGE ( 'NONE', *, *, #18604, .T. ) ;
#21769=ORIENTED_EDGE ( 'NONE', *, *, #20610, .F. ) ;
#21776=ADVANCED_FACE ( 'NONE', ( #17320 ), #20125, .F. ) ;
#21782=CYLINDRICAL_SURFACE ( 'NONE', #12200, 1.500000000000001332 ) ;
#21783=ORIENTED_EDGE ( 'NONE', *, *, #11991, .F. ) ;
#21787=ORIENTED_EDGE ( 'NONE', *, *, #19834, .F. ) ;
#21788=DIRECTION ( 'NONE',  ( -0.000000000000000000, -0.000000000000000000, 1.000000000000000000 ) ) ;
#21796=DIRECTION ( 'NONE',  ( 1.000000000000000000, 0.000000000000000000, 0.000000000000000000 ) ) ;
#21797=ORIENTED_EDGE ( 'NONE', *, *, #15937, .F. ) ;
#21798=ORIENTED_EDGE ( 'NONE', *, *, #19783, .F. ) ;
#21802=VERTEX_POINT ( 'NONE', #2933 ) ;
#21808=LINE ( 'NONE', #9095, #6881 ) ;
#21814=VERTEX_POINT ( 'NONE', #23325 ) ;
#21822=CARTESIAN_POINT ( 'NONE',  ( -41.00000000000000000, 4.000000000000000888, 10.49999999999999822 ) ) ;
#21834=EDGE_CURVE ( 'NONE', #12069, #3216, #13468, .T. ) ;
#21840=ORIENTED_EDGE ( 'NONE', *, *, #17150, .F. ) ;
#21851=CARTESIAN_POINT ( 'NONE',  ( 41.58578643762692195, -26.57671364288190219, 12.00000000000000000 ) ) ;
#21852=EDGE_LOOP ( 'NONE', ( #9595, #21884, #23311, #1871 ) ) ;
#21858=DIRECTION ( 'NONE',  ( -0.000000000000000000, -0.000000000000000000, -1.000000000000000000 ) ) ;
#21859=CARTESIAN_POINT ( 'NONE',  ( 2.454813078130514813E-15, 16.67999999999999972, 13.50000000000000178 ) ) ;
#21860=EDGE_CURVE ( 'NONE', #16259, #19489, #14377, .T. ) ;
#21867=VERTEX_POINT ( 'NONE', #14267 ) ;
#21872=LINE ( 'NONE', #2842, #3053 ) ;
#21879=EDGE_LOOP ( 'NONE', ( #10298, #17785, #5069, #18775 ) ) ;
#21881=LINE ( 'NONE', #4949, #17623 ) ;
#21884=ORIENTED_EDGE ( 'NONE', *, *, #4700, .T. ) ;
#21886=VERTEX_POINT ( 'NONE', #4898 ) ;
#21888=CARTESIAN_POINT ( 'NONE',  ( -41.00000000000000000, -5.000000000000000888, 9.500000000000000000 ) ) ;
#21899=PLANE ( 'NONE',  #14776 ) ;
#21900=CARTESIAN_POINT ( 'NONE',  ( 40.00000000000000000, 0.000000000000000000, 11.00000000000000000 ) ) ;
#21901=CARTESIAN_POINT ( 'NONE',  ( -41.51716637648671338, 25.94562225875360539, 12.00000000000000000 ) ) ;
#21910=CIRCLE ( 'NONE', #12154, 8.000000000000003553 ) ;
#21916=CIRCLE ( 'NONE', #12541, 1.500000000000001332 ) ;
#21932=CARTESIAN_POINT ( 'NONE',  ( -20.84999999999999787, -16.67999999999985050, 13.50000000000000178 ) ) ;
#21935=VECTOR ( 'NONE', #9472, 1000.000000000000000 ) ;
#21946=EDGE_CURVE ( 'NONE', #11259, #21867, #1579, .T. ) ;
#21956=AXIS2_PLACEMENT_3D ( 'NONE', #926, #8350, #17760 ) ;
#21962=VERTEX_POINT ( 'NONE', #7181 ) ;
#21973=CARTESIAN_POINT ( 'NONE',  ( -1.999999999999994449, -45.00000000000000000, 3.000000000000002665 ) ) ;
#21975=VERTEX_POINT ( 'NONE', #19015 ) ;
#21982=AXIS2_PLACEMENT_3D ( 'NONE', #18990, #6279, #13606 ) ;
#21988=ORIENTED_EDGE ( 'NONE', *, *, #6153, .F. ) ;
#21989=CARTESIAN_POINT ( 'NONE',  ( 41.58578643762692195, 26.57671364288191285, 12.00000000000000000 ) ) ;
#21996=ORIENTED_EDGE ( 'NONE', *, *, #10656, .F. ) ;
#21998=CARTESIAN_POINT ( 'NONE',  ( -29.00000000000000000, -29.49999999999999645, 11.50000000000000000 ) ) ;
#22004=CIRCLE ( 'NONE', #4491, 1.000000000000000888 ) ;
#22012=CARTESIAN_POINT ( 'NONE',  ( 31.10231664966676846, -45.36128193761570770, 11.00000000000000000 ) ) ;
#22017=ORIENTED_EDGE ( 'NONE', *, *, #18604, .F. ) ;
#22023=LINE ( 'NONE', #8937, #269 ) ;
#22024=AXIS2_PLACEMENT_3D ( 'NONE', #19752, #6568, #17792 ) ;
#22028=EDGE_LOOP ( 'NONE', ( #23894, #17676 ) ) ;
#22030=ORIENTED_EDGE ( 'NONE', *, *, #22910, .T. ) ;
#22031=( BOUNDED_CURVE ( )  B_SPLINE_CURVE ( 3, ( #6539, #21989, #14293, #799 ),
 .UNSPECIFIED., .F., .F. ) 
 B_SPLINE_CURVE_WITH_KNOTS ( ( 4, 4 ),
 ( 1.570796326794896558, 3.141592653589793116 ),
 .UNSPECIFIED. ) 
 CURVE ( )  GEOMETRIC_REPRESENTATION_ITEM ( )  RATIONAL_B_SPLINE_CURVE ( ( 1.000000000000000000, 0.8047378541243649375, 0.8047378541243649375, 1.000000000000000000 ) ) 
 REPRESENTATION_ITEM ( '' )  );
#22035=DIRECTION ( 'NONE',  ( 0.000000000000000000, 0.000000000000000000, 1.000000000000000000 ) ) ;
#22057=CIRCLE ( 'NONE', #2574, 1.000000000000000888 ) ;
#22059=VECTOR ( 'NONE', #7909, 1000.000000000000000 ) ;
#22074=CARTESIAN_POINT ( 'NONE',  ( -20.84999999999999787, 16.67999999999985405, 13.00000000000000178 ) ) ;
#22077=DIRECTION ( 'NONE',  ( -0.000000000000000000, 0.000000000000000000, 1.000000000000000000 ) ) ;
#22078=ORIENTED_EDGE ( 'NONE', *, *, #1443, .T. ) ;
#22080=ORIENTED_EDGE ( 'NONE', *, *, #19250, .F. ) ;
#22088=CARTESIAN_POINT ( 'NONE',  ( -20.84999999999999787, 16.67999999999985405, 14.50000000000000000 ) ) ;
#22107=CARTESIAN_POINT ( 'NONE',  ( 0.000000000000000000, 0.000000000000000000, 11.00000000000000000 ) ) ;
#22110=DIRECTION ( 'NONE',  ( 0.000000000000000000, 0.000000000000000000, 1.000000000000000000 ) ) ;
#22117=TOROIDAL_SURFACE ( 'NONE', #13919, 3.999999999999999112, 1.000000000000000000 ) ;
#22123=CARTESIAN_POINT ( 'NONE',  ( 29.00000000000000000, 29.50000000000000355, 11.50000000000000000 ) ) ;
#22129=VERTEX_POINT ( 'NONE', #17287 ) ;
#22133=LINE ( 'NONE', #16970, #21142 ) ;
#22142=CIRCLE ( 'NONE', #8489, 1.000000000000000888 ) ;
#22150=FACE_OUTER_BOUND ( 'NONE', #11134, .T. ) ;
#22154=EDGE_LOOP ( 'NONE', ( #20295, #4668 ) ) ;
#22156=FACE_BOUND ( 'NONE', #15619, .T. ) ;
#22159=CARTESIAN_POINT ( 'NONE',  ( 39.00000000000000000, -29.49999999999999645, 11.00000000000000000 ) ) ;
#22169=VERTEX_POINT ( 'NONE', #9825 ) ;
#22170=EDGE_LOOP ( 'NONE', ( #5678, #22251, #13140, #3397 ) ) ;
#22172=DIRECTION ( 'NONE',  ( 0.000000000000000000, -0.000000000000000000, -1.000000000000000000 ) ) ;
#22174=EDGE_CURVE ( 'NONE', #8062, #17642, #1057, .T. ) ;
#22175=( BOUNDED_CURVE ( )  B_SPLINE_CURVE ( 3, ( #1129, #8433, #21851, #19681 ),
 .UNSPECIFIED., .F., .T. ) 
 B_SPLINE_CURVE_WITH_KNOTS ( ( 4, 4 ),
 ( 0.000000000000000000, 1.570796326794897224 ),
 .UNSPECIFIED. ) 
 CURVE ( )  GEOMETRIC_REPRESENTATION_ITEM ( )  RATIONAL_B_SPLINE_CURVE ( ( 1.000000000000000000, 0.8047378541243649375, 0.8047378541243649375, 1.000000000000000000 ) ) 
 REPRESENTATION_ITEM ( '' )  );
#22177=DIRECTION ( 'NONE',  ( -0.000000000000000000, -0.000000000000000000, -1.000000000000000000 ) ) ;
#22178=DIRECTION ( 'NONE',  ( 1.000000000000000000, 0.000000000000000000, 0.000000000000000000 ) ) ;
#22179=CARTESIAN_POINT ( 'NONE',  ( 41.00000000000000000, -4.000000000000015099, 9.500000000000000000 ) ) ;
#22180=DIRECTION ( 'NONE',  ( -0.000000000000000000, -0.000000000000000000, -1.000000000000000000 ) ) ;
#22181=DIRECTION ( 'NONE',  ( 1.000000000000000000, 0.000000000000000000, 0.000000000000000000 ) ) ;
#22185=EDGE_LOOP ( 'NONE', ( #8238, #20868, #4232, #20795, #8188 ) ) ;
#22191=LINE ( 'NONE', #8761, #4404 ) ;
#22192=CARTESIAN_POINT ( 'NONE',  ( -41.50000000000000000, -28.80990663662250739, 12.00000000000000000 ) ) ;
#22193=ORIENTED_EDGE ( 'NONE', *, *, #7085, .F. ) ;
#22206=DIRECTION ( 'NONE',  ( -1.000000000000000000, -0.000000000000000000, 0.000000000000000000 ) ) ;
#22222=FACE_OUTER_BOUND ( 'NONE', #22606, .T. ) ;
#22224=ORIENTED_EDGE ( 'NONE', *, *, #13051, .F. ) ;
#22231=ORIENTED_EDGE ( 'NONE', *, *, #4579, .T. ) ;
#22236=CARTESIAN_POINT ( 'NONE',  ( -41.50000000000000000, 28.80990663662250739, 12.00000000000000000 ) ) ;
#22240=DIRECTION ( 'NONE',  ( 0.000000000000000000, -0.000000000000000000, -1.000000000000000000 ) ) ;
#22243=EDGE_CURVE ( 'NONE', #3705, #7597, #17391, .T. ) ;
#22245=CARTESIAN_POINT ( 'NONE',  ( 37.00000000000000711, 29.50000000000000355, 11.50000000000000000 ) ) ;
#22251=ORIENTED_EDGE ( 'NONE', *, *, #22302, .F. ) ;
#22257=ORIENTED_EDGE ( 'NONE', *, *, #5132, .F. ) ;
#22285=LINE ( 'NONE', #12871, #19420 ) ;
#22286=CARTESIAN_POINT ( 'NONE',  ( -34.00000000000000000, -3.999999999999999112, 10.49999999999999822 ) ) ;
#22287=DIRECTION ( 'NONE',  ( 0.000000000000000000, 0.000000000000000000, 1.000000000000000000 ) ) ;
#22290=ADVANCED_FACE ( 'NONE', ( #3106 ), #1280, .T. ) ;
#22298=AXIS2_PLACEMENT_3D ( 'NONE', #1230, #4904, #6842 ) ;
#22302=EDGE_CURVE ( 'NONE', #19325, #18986, #22023, .T. ) ;
#22303=EDGE_CURVE ( 'NONE', #7495, #17534, #3218, .T. ) ;
#22334=EDGE_CURVE ( 'NONE', #8265, #16259, #22858, .T. ) ;
#22339=CIRCLE ( 'NONE', #11783, 5.999999999999998224 ) ;
#22344=DIRECTION ( 'NONE',  ( 0.000000000000000000, 0.000000000000000000, 1.000000000000000000 ) ) ;
#22358=VECTOR ( 'NONE', #22993, 1000.000000000000000 ) ;
#22370=CARTESIAN_POINT ( 'NONE',  ( 33.99999999999998579, 4.999999999999985789, 11.00000000000000000 ) ) ;
#22372=DIRECTION ( 'NONE',  ( -1.000000000000000000, 2.600433232233976523E-16, 0.000000000000000000 ) ) ;
#22374=ORIENTED_EDGE ( 'NONE', *, *, #12940, .F. ) ;
#22375=ORIENTED_EDGE ( 'NONE', *, *, #14565, .F. ) ;
#22381=DIRECTION ( 'NONE',  ( 1.000000000000000000, 0.000000000000000000, 0.000000000000000000 ) ) ;
#22383=AXIS2_PLACEMENT_3D ( 'NONE', #5049, #12820, #12461 ) ;
#22388=ORIENTED_EDGE ( 'NONE', *, *, #5531, .F. ) ;
#22393=CARTESIAN_POINT ( 'NONE',  ( -41.00000000000000000, 6.000000000000000888, 11.00000000000000000 ) ) ;
#22394=CIRCLE ( 'NONE', #11069, 1.000000000000000888 ) ;
#22407=EDGE_LOOP ( 'NONE', ( #5838, #4332, #7816, #91 ) ) ;
#22408=VERTEX_POINT ( 'NONE', #8579 ) ;
#22409=CARTESIAN_POINT ( 'NONE',  ( 33.99999999999998579, -1.387778780781445676E-14, 12.00000000000000000 ) ) ;
#22411=CARTESIAN_POINT ( 'NONE',  ( 33.99999999999998579, -5.000000000000013323, 10.49999999999999822 ) ) ;
#22413=ORIENTED_EDGE ( 'NONE', *, *, #7159, .T. ) ;
#22419=CARTESIAN_POINT ( 'NONE',  ( 31.10231664966676846, -45.36128193761570770, 11.00000000000000000 ) ) ;
#22426=DIRECTION ( 'NONE',  ( 1.000000000000000000, 0.000000000000000000, 0.000000000000000000 ) ) ;
#22428=DIRECTION ( 'NONE',  ( -0.8757121056631642642, 0.4828336235133043886, -0.000000000000000000 ) ) ;
#22431=AXIS2_PLACEMENT_3D ( 'NONE', #15700, #15572, #6452 ) ;
#22435=ORIENTED_EDGE ( 'NONE', *, *, #1443, .F. ) ;
#22442=ORIENTED_EDGE ( 'NONE', *, *, #18212, .T. ) ;
#22454=CARTESIAN_POINT ( 'NONE',  ( -0.9830802669677229932, 45.00000000000000000, 3.000000000000002665 ) ) ;
#22462=AXIS2_PLACEMENT_3D ( 'NONE', #16331, #10718, #16098 ) ;
#22473=AXIS2_PLACEMENT_3D ( 'NONE', #21664, #18236, #14556 ) ;
#22476=EDGE_CURVE ( 'NONE', #13857, #2378, #15430, .T. ) ;
#22504=ORIENTED_EDGE ( 'NONE', *, *, #11949, .T. ) ;
#22508=CARTESIAN_POINT ( 'NONE',  ( 42.00000000000000000, -26.82133436441678853, 0.000000000000000000 ) ) ;
#22512=CARTESIAN_POINT ( 'NONE',  ( -30.31394790604173650, 39.41330121100982353, 11.00000000000000000 ) ) ;
#22516=DIRECTION ( 'NONE',  ( -0.000000000000000000, -1.000000000000000000, -0.000000000000000000 ) ) ;
#22517=ADVANCED_FACE ( 'NONE', ( #11231 ), #18908, .T. ) ;
#22534=DIRECTION ( 'NONE',  ( -1.000000000000000000, 0.000000000000000000, 0.000000000000000000 ) ) ;
#22535=AXIS2_PLACEMENT_3D ( 'NONE', #9324, #3743, #16545 ) ;
#22543=CYLINDRICAL_SURFACE ( 'NONE', #11848, 1.000000000000002442 ) ;
#22545=ORIENTED_EDGE ( 'NONE', *, *, #12393, .T. ) ;
#22546=ORIENTED_EDGE ( 'NONE', *, *, #7133, .F. ) ;
#22549=ORIENTED_EDGE ( 'NONE', *, *, #15724, .F. ) ;
#22564=ORIENTED_EDGE ( 'NONE', *, *, #22243, .T. ) ;
#22576=CYLINDRICAL_SURFACE ( 'NONE', #20742, 1.999999999999994449 ) ;
#22584=CARTESIAN_POINT ( 'NONE',  ( 41.00000000000000000, 3.999999999999987121, 8.500000000000000000 ) ) ;
#22585=DIRECTION ( 'NONE',  ( 0.000000000000000000, 0.000000000000000000, -1.000000000000000000 ) ) ;
#22591=DIRECTION ( 'NONE',  ( 0.000000000000000000, 0.000000000000000000, 1.000000000000000000 ) ) ;
#22602=DIRECTION ( 'NONE',  ( 1.000000000000000000, 0.000000000000000000, 0.000000000000000000 ) ) ;
#22604=ORIENTED_EDGE ( 'NONE', *, *, #5463, .F. ) ;
#22605=CIRCLE ( 'NONE', #17143, 5.099999999999996980 ) ;
#22606=EDGE_LOOP ( 'NONE', ( #23240, #3452, #6311, #14731 ) ) ;
#22607=EDGE_LOOP ( 'NONE', ( #12145, #22941 ) ) ;
#22608=DIRECTION ( 'NONE',  ( -0.000000000000000000, 0.000000000000000000, -1.000000000000000000 ) ) ;
#22611=ORIENTED_EDGE ( 'NONE', *, *, #2218, .F. ) ;
#22616=PLANE ( 'NONE',  #8234 ) ;
#22618=CARTESIAN_POINT ( 'NONE',  ( 42.00000000000000000, -26.82133436441678853, 12.00000000000000000 ) ) ;
#22620=VECTOR ( 'NONE', #20471, 1000.000000000000000 ) ;
#22647=ORIENTED_EDGE ( 'NONE', *, *, #4369, .F. ) ;
#22655=EDGE_LOOP ( 'NONE', ( #10922, #22388, #5719, #22435 ) ) ;
#22662=CYLINDRICAL_SURFACE ( 'NONE', #600, 8.000000000000003553 ) ;
#22667=DIRECTION ( 'NONE',  ( -0.000000000000000000, -0.000000000000000000, -1.000000000000000000 ) ) ;
#22669=DIRECTION ( 'NONE',  ( -0.000000000000000000, -0.000000000000000000, -1.000000000000000000 ) ) ;
#22673=EDGE_CURVE ( 'NONE', #15508, #20363, #8313, .T. ) ;
#22681=ORIENTED_EDGE ( 'NONE', *, *, #6799, .F. ) ;
#22688=AXIS2_PLACEMENT_3D ( 'NONE', #16675, #17030, #17145 ) ;
#22715=CIRCLE ( 'NONE', #18058, 1.000000000000000888 ) ;
#22719=DIRECTION ( 'NONE',  ( 2.600433232233976523E-16, 1.000000000000000000, 0.000000000000000000 ) ) ;
#22730=AXIS2_PLACEMENT_3D ( 'NONE', #20073, #19721, #5065 ) ;
#22737=EDGE_CURVE ( 'NONE', #22129, #8481, #21656, .T. ) ;
#22757=ORIENTED_EDGE ( 'NONE', *, *, #21102, .F. ) ;
#22770=DIRECTION ( 'NONE',  ( -1.000000000000000000, 0.000000000000000000, 0.000000000000000000 ) ) ;
#22774=ORIENTED_EDGE ( 'NONE', *, *, #1836, .T. ) ;
#22775=CARTESIAN_POINT ( 'NONE',  ( 41.00000000000000000, -6.000000000000015099, 12.00000000000000000 ) ) ;
#22779=CARTESIAN_POINT ( 'NONE',  ( -2.983080266967717442, 45.00000000000000000, 0.000000000000000000 ) ) ;
#22782=AXIS2_PLACEMENT_3D ( 'NONE', #22419, #12998, #3972 ) ;
#22783=DIRECTION ( 'NONE',  ( 0.000000000000000000, 1.000000000000000000, 0.000000000000000000 ) ) ;
#22790=VERTEX_POINT ( 'NONE', #12342 ) ;
#22793=CIRCLE ( 'NONE', #16150, 20.85000000000000142 ) ;
#22804=ORIENTED_EDGE ( 'NONE', *, *, #10823, .F. ) ;
#22808=CARTESIAN_POINT ( 'NONE',  ( -42.00000000000000000, -26.82133436441678853, 11.00000000000000000 ) ) ;
#22823=CIRCLE ( 'NONE', #10763, 5.099999999999996980 ) ;
#22824=ORIENTED_EDGE ( 'NONE', *, *, #13958, .T. ) ;
#22828=DIRECTION ( 'NONE',  ( 0.000000000000000000, -0.000000000000000000, -1.000000000000000000 ) ) ;
#22837=EDGE_LOOP ( 'NONE', ( #8933, #12552, #22757, #21798 ) ) ;
#22846=DIRECTION ( 'NONE',  ( 1.000000000000000000, 0.000000000000000000, 0.000000000000000000 ) ) ;
#22858=CIRCLE ( 'NONE', #19749, 1.999999999999994449 ) ;
#22881=CARTESIAN_POINT ( 'NONE',  ( 29.00000000000000000, 29.50000000000000355, 12.00000000000000000 ) ) ;
#22883=FACE_OUTER_BOUND ( 'NONE', #12736, .T. ) ;
#22884=ORIENTED_EDGE ( 'NONE', *, *, #3237, .T. ) ;
#22888=EDGE_LOOP ( 'NONE', ( #15138, #14134, #23261, #8237 ) ) ;
#22889=EDGE_CURVE ( 'NONE', #20146, #15114, #12677, .T. ) ;
#22894=CARTESIAN_POINT ( 'NONE',  ( 41.50000000000000000, -28.80990663662250739, 0.000000000000000000 ) ) ;
#22897=FACE_OUTER_BOUND ( 'NONE', #20480, .T. ) ;
#22898=DIRECTION ( 'NONE',  ( 1.000000000000000000, 0.000000000000000000, 0.000000000000000000 ) ) ;
#22901=VERTEX_POINT ( 'NONE', #6512 ) ;
#22910=EDGE_CURVE ( 'NONE', #6894, #14074, #22057, .T. ) ;
#22926=EDGE_LOOP ( 'NONE', ( #21073, #17229, #11328, #4423 ) ) ;
#22935=ADVANCED_FACE ( 'NONE', ( #21754 ), #19130, .T. ) ;
#22941=ORIENTED_EDGE ( 'NONE', *, *, #19250, .T. ) ;
#22947=CARTESIAN_POINT ( 'NONE',  ( -39.00000000000000000, -28.80990663662251450, 11.00000000000000000 ) ) ;
#22950=DIRECTION ( 'NONE',  ( -1.000000000000000000, 0.000000000000000000, 0.000000000000000000 ) ) ;
#22955=DIRECTION ( 'NONE',  ( -0.000000000000000000, 0.000000000000000000, -1.000000000000000000 ) ) ;
#22964=CARTESIAN_POINT ( 'NONE',  ( -31.10231664966676846, 45.36128193761570770, 12.00000000000000000 ) ) ;
#22976=EDGE_LOOP ( 'NONE', ( #20539, #2296, #204 ) ) ;
#22993=DIRECTION ( 'NONE',  ( 1.000000000000000000, -2.600433232233976523E-16, 0.000000000000000000 ) ) ;
#22999=AXIS2_PLACEMENT_3D ( 'NONE', #12436, #19538, #14156 ) ;
#23016=EDGE_LOOP ( 'NONE', ( #3069, #9035, #5154, #2283 ) ) ;
#23032=ADVANCED_FACE ( 'NONE', ( #18323 ), #8456, .F. ) ;
#23041=CARTESIAN_POINT ( 'NONE',  ( -34.00000000000000000, -3.999999999999999112, 9.500000000000000000 ) ) ;
#23044=DIRECTION ( 'NONE',  ( 0.000000000000000000, 0.000000000000000000, 1.000000000000000000 ) ) ;
#23048=ORIENTED_EDGE ( 'NONE', *, *, #2298, .F. ) ;
#23054=ORIENTED_EDGE ( 'NONE', *, *, #15449, .T. ) ;
#23058=AXIS2_PLACEMENT_3D ( 'NONE', #17804, #12157, #2915 ) ;
#23072=LINE ( 'NONE', #13799, #7775 ) ;
#23080=VECTOR ( 'NONE', #10781, 1000.000000000000227 ) ;
#23095=VECTOR ( 'NONE', #4994, 1000.000000000000000 ) ;
#23096=CONICAL_SURFACE ( 'NONE', #12557, 1.999999999999994449, 1.029744258676653201 ) ;
#23101=VERTEX_POINT ( 'NONE', #15698 ) ;
#23102=TOROIDAL_SURFACE ( 'NONE', #1683, 2.000000000000000000, 1.000000000000000000 ) ;
#23118=ORIENTED_EDGE ( 'NONE', *, *, #18306, .F. ) ;
#23123=EDGE_CURVE ( 'NONE', #3216, #15508, #8012, .T. ) ;
#23124=AXIS2_PLACEMENT_3D ( 'NONE', #1982, #3573, #15140 ) ;
#23127=EDGE_LOOP ( 'NONE', ( #11198, #18149, #14109, #776 ) ) ;
#23139=ADVANCED_FACE ( 'NONE', ( #23412 ), #11916, .T. ) ;
#23144=EDGE_LOOP ( 'NONE', ( #15879, #1858, #20986, #9765 ) ) ;
#23163=CARTESIAN_POINT ( 'NONE',  ( -42.00000000000000000, -6.000000000000000888, 12.00000000000000000 ) ) ;
#23165=EDGE_CURVE ( 'NONE', #21057, #3216, #1789, .T. ) ;
#23166=DIRECTION ( 'NONE',  ( -1.000000000000000000, 2.600433232233976523E-16, -0.000000000000000000 ) ) ;
#23168=EDGE_LOOP ( 'NONE', ( #5710, #295, #15144, #22257 ) ) ;
#23174=CARTESIAN_POINT ( 'NONE',  ( -27.70933665152131198, 40.41277845351217479, 11.00000000000000000 ) ) ;
#23182=AXIS2_PLACEMENT_3D ( 'NONE', #23344, #14394, #20507 ) ;
#23186=CIRCLE ( 'NONE', #12641, 11.00000000000001066 ) ;
#23190=CARTESIAN_POINT ( 'NONE',  ( 37.00000000000000711, 29.50000000000000355, 12.00000000000000000 ) ) ;
#23192=CARTESIAN_POINT ( 'NONE',  ( 42.00000000000000000, -4.000000000000015099, 9.500000000000000000 ) ) ;
#23195=VECTOR ( 'NONE', #1085, 1000.000000000000000 ) ;
#23196=CARTESIAN_POINT ( 'NONE',  ( -41.50000000000000000, -28.80990663662250739, 12.00000000000000000 ) ) ;
#23209=CARTESIAN_POINT ( 'NONE',  ( 40.00000000000000000, 28.80990663662251450, 0.000000000000000000 ) ) ;
#23214=VECTOR ( 'NONE', #21376, 1000.000000000000000 ) ;
#23225=DIRECTION ( 'NONE',  ( -1.000000000000000000, 0.000000000000000000, 0.000000000000000000 ) ) ;
#23228=AXIS2_PLACEMENT_3D ( 'NONE', #20516, #19045, #18787 ) ;
#23229=ORIENTED_EDGE ( 'NONE', *, *, #10244, .F. ) ;
#23231=ORIENTED_EDGE ( 'NONE', *, *, #834, .T. ) ;
#23240=ORIENTED_EDGE ( 'NONE', *, *, #11206, .T. ) ;
#23250=VERTEX_POINT ( 'NONE', #17420 ) ;
#23260=EDGE_CURVE ( 'NONE', #19153, #1596, #21808, .T. ) ;
#23261=ORIENTED_EDGE ( 'NONE', *, *, #7581, .T. ) ;
#23266=DIRECTION ( 'NONE',  ( -0.000000000000000000, -0.000000000000000000, -1.000000000000000000 ) ) ;
#23273=ORIENTED_EDGE ( 'NONE', *, *, #8251, .T. ) ;
#23289=EDGE_CURVE ( 'NONE', #7597, #15489, #3383, .T. ) ;
#23290=EDGE_LOOP ( 'NONE', ( #8573, #2077, #18536, #9894 ) ) ;
#23298=DIRECTION ( 'NONE',  ( -0.000000000000000000, -0.000000000000000000, -1.000000000000000000 ) ) ;
#23300=VERTEX_POINT ( 'NONE', #3256 ) ;
#23311=ORIENTED_EDGE ( 'NONE', *, *, #14008, .F. ) ;
#23317=AXIS2_PLACEMENT_3D ( 'NONE', #3614, #6930, #3495 ) ;
#23325=CARTESIAN_POINT ( 'NONE',  ( 23.90000000000000568, -29.50000000000000355, 0.000000000000000000 ) ) ;
#23329=FACE_OUTER_BOUND ( 'NONE', #10071, .T. ) ;
#23336=DIRECTION ( 'NONE',  ( 1.000000000000000000, 0.000000000000000000, 0.000000000000000000 ) ) ;
#23341=EDGE_CURVE ( 'NONE', #8229, #17123, #23647, .T. ) ;
#23344=CARTESIAN_POINT ( 'NONE',  ( -21.84999999999999787, -16.67999999999985050, 13.00000000000000178 ) ) ;
#23354=EDGE_CURVE ( 'NONE', #5912, #19325, #13090, .T. ) ;
#23359=FACE_BOUND ( 'NONE', #2285, .T. ) ;
#23364=ORIENTED_EDGE ( 'NONE', *, *, #4768, .F. ) ;
#23365=DIRECTION ( 'NONE',  ( 0.000000000000000000, 0.000000000000000000, -1.000000000000000000 ) ) ;
#23370=CYLINDRICAL_SURFACE ( 'NONE', #11014, 1.000000000000000888 ) ;
#23372=ORIENTED_EDGE ( 'NONE', *, *, #10449, .F. ) ;
#23380=ORIENTED_EDGE ( 'NONE', *, *, #2757, .F. ) ;
#23382=DIRECTION ( 'NONE',  ( 1.000000000000000000, 3.469446951953611033E-15, 0.000000000000000000 ) ) ;
#23383=ADVANCED_FACE ( 'NONE', ( #23655 ), #21687, .T. ) ;
#23385=CARTESIAN_POINT ( 'NONE',  ( -41.00000000000000000, 6.000000000000000888, 11.00000000000000000 ) ) ;
#23404=ORIENTED_EDGE ( 'NONE', *, *, #7213, .T. ) ;
#23412=FACE_OUTER_BOUND ( 'NONE', #10371, .T. ) ;
#23420=DIRECTION ( 'NONE',  ( -0.000000000000000000, -0.000000000000000000, -1.000000000000000000 ) ) ;
#23421=LINE ( 'NONE', #12038, #1697 ) ;
#23425=EDGE_LOOP ( 'NONE', ( #19479, #11105, #15389, #21573 ) ) ;
#23435=ADVANCED_FACE ( 'NONE', ( #1906 ), #5701, .F. ) ;
#23440=EDGE_CURVE ( 'NONE', #17472, #8169, #5806, .T. ) ;
#23441=EDGE_LOOP ( 'NONE', ( #15642, #20254, #6859, #1561 ) ) ;
#23443=CARTESIAN_POINT ( 'NONE',  ( 41.00000000000000000, -4.000000000000015099, 8.500000000000000000 ) ) ;
#23445=CYLINDRICAL_SURFACE ( 'NONE', #4339, 1.000000000000000888 ) ;
#23448=CARTESIAN_POINT ( 'NONE',  ( 41.00000000000000000, 4.999999999999986677, 11.00000000000000000 ) ) ;
#23454=DIRECTION ( 'NONE',  ( -1.000000000000000000, 0.000000000000000000, 0.000000000000000000 ) ) ;
#23474=DIRECTION ( 'NONE',  ( 1.000000000000000000, 0.000000000000000000, 0.000000000000000000 ) ) ;
#23479=DIRECTION ( 'NONE',  ( -0.000000000000000000, 0.000000000000000000, 1.000000000000000000 ) ) ;
#23483=EDGE_CURVE ( 'NONE', #21197, #19750, #3742, .T. ) ;
#23488=EDGE_LOOP ( 'NONE', ( #1042, #23966, #5800, #22804 ) ) ;
#23494=AXIS2_PLACEMENT_3D ( 'NONE', #9043, #13068, #18690 ) ;
#23500=ORIENTED_EDGE ( 'NONE', *, *, #20841, .T. ) ;
#23501=DIRECTION ( 'NONE',  ( 0.000000000000000000, 0.000000000000000000, 1.000000000000000000 ) ) ;
#23503=FACE_OUTER_BOUND ( 'NONE', #22607, .T. ) ;
#23504=CARTESIAN_POINT ( 'NONE',  ( -31.10231664966676846, -45.36128193761570770, 11.00000000000000000 ) ) ;
#23509=AXIS2_PLACEMENT_3D ( 'NONE', #22107, #10486, #9135 ) ;
#23510=AXIS2_PLACEMENT_3D ( 'NONE', #18007, #18361, #1649 ) ;
#23528=AXIS2_PLACEMENT_3D ( 'NONE', #10375, #4909, #19794 ) ;
#23535=VECTOR ( 'NONE', #1892, 1000.000000000000000 ) ;
#23537=DIRECTION ( 'NONE',  ( 0.000000000000000000, 0.000000000000000000, 1.000000000000000000 ) ) ;
#23538=CARTESIAN_POINT ( 'NONE',  ( -34.10000000000000142, 29.49999999999999645, 12.00000000000000000 ) ) ;
#23548=AXIS2_PLACEMENT_3D ( 'NONE', #6000, #11219, #1962 ) ;
#23549=ORIENTED_EDGE ( 'NONE', *, *, #16550, .F. ) ;
#23551=AXIS2_PLACEMENT_3D ( 'NONE', #3183, #18087, #1601 ) ;
#23554=DIRECTION ( 'NONE',  ( 1.000000000000000000, -2.600433232233976523E-16, 0.000000000000000000 ) ) ;
#23559=VECTOR ( 'NONE', #18522, 1000.000000000000000 ) ;
#23560=DIRECTION ( 'NONE',  ( -1.000000000000000000, 0.000000000000000000, 0.000000000000000000 ) ) ;
#23569=DIRECTION ( 'NONE',  ( -1.000000000000000000, 0.000000000000000000, 0.000000000000000000 ) ) ;
#23571=VECTOR ( 'NONE', #21858, 1000.000000000000000 ) ;
#23585=LINE ( 'NONE', #23703, #282 ) ;
#23595=EDGE_LOOP ( 'NONE', ( #15599, #20995 ) ) ;
#23599=DIRECTION ( 'NONE',  ( 0.7071067811865660024, 8.659560562355159656E-17, -0.7071067811865291430 ) ) ;
#23619=ORIENTED_EDGE ( 'NONE', *, *, #6826, .F. ) ;
#23623=DIRECTION ( 'NONE',  ( 1.000000000000000000, 2.600433232233976523E-16, -0.000000000000000000 ) ) ;
#23626=DIRECTION ( 'NONE',  ( 1.000000000000000000, 0.000000000000000000, 0.000000000000000000 ) ) ;
#23634=CARTESIAN_POINT ( 'NONE',  ( 41.00000000000000000, -5.000000000000015099, 10.49999999999999822 ) ) ;
#23647=CIRCLE ( 'NONE', #8019, 1.000000000000000888 ) ;
#23648=CARTESIAN_POINT ( 'NONE',  ( 2.454813078130514813E-15, 16.67999999999999972, 13.00000000000000178 ) ) ;
#23655=FACE_OUTER_BOUND ( 'NONE', #9210, .T. ) ;
#23657=CARTESIAN_POINT ( 'NONE',  ( 29.99999999999998934, -1.387778780781445676E-14, 10.49999999999999822 ) ) ;
#23660=EDGE_CURVE ( 'NONE', #11172, #5011, #11942, .T. ) ;
#23663=CARTESIAN_POINT ( 'NONE',  ( 2.024999999999999911, -45.00000000000000000, 0.000000000000000000 ) ) ;
#23670=DIRECTION ( 'NONE',  ( 0.000000000000000000, 1.000000000000000000, 0.000000000000000000 ) ) ;
#23693=DIRECTION ( 'NONE',  ( 0.000000000000000000, -0.000000000000000000, -1.000000000000000000 ) ) ;
#23703=CARTESIAN_POINT ( 'NONE',  ( 20.85000000000000497, 16.67999999999999972, 14.50000000000000000 ) ) ;
#23711=ORIENTED_EDGE ( 'NONE', *, *, #16794, .F. ) ;
#23714=ADVANCED_FACE ( 'NONE', ( #20646 ), #9982, .T. ) ;
#23720=ORIENTED_EDGE ( 'NONE', *, *, #7354, .T. ) ;
#23722=DIRECTION ( 'NONE',  ( -1.000000000000000000, 2.600433232233976523E-16, 0.000000000000000000 ) ) ;
#23736=EDGE_CURVE ( 'NONE', #11854, #13833, #7634, .T. ) ;
#23740=VECTOR ( 'NONE', #10243, 1000.000000000000000 ) ;
#23742=CARTESIAN_POINT ( 'NONE',  ( 20.99999999999999645, 29.50000000000000355, 12.00000000000000000 ) ) ;
#23746=DIRECTION ( 'NONE',  ( -0.000000000000000000, -0.000000000000000000, -1.000000000000000000 ) ) ;
#23750=CARTESIAN_POINT ( 'NONE',  ( -0.9830802669677229932, 45.00000000000000000, 3.000000000000002665 ) ) ;
#23760=DIRECTION ( 'NONE',  ( 0.000000000000000000, 0.000000000000000000, 1.000000000000000000 ) ) ;
#23767=VECTOR ( 'NONE', #12847, 1000.000000000000227 ) ;
#23781=CARTESIAN_POINT ( 'NONE',  ( -37.00000000000000711, 29.49999999999999645, 11.50000000000000000 ) ) ;
#23787=ADVANCED_FACE ( 'NONE', ( #5877 ), #16242, .T. ) ;
#23794=CARTESIAN_POINT ( 'NONE',  ( -41.00000000000000000, -4.000000000000000888, 10.49999999999999822 ) ) ;
#23797=AXIS2_PLACEMENT_3D ( 'NONE', #22192, #7171, #1569 ) ;
#23801=ORIENTED_EDGE ( 'NONE', *, *, #21102, .T. ) ;
#23807=CARTESIAN_POINT ( 'NONE',  ( -34.00000000000000000, -3.851859888774471706E-31, 10.49999999999999822 ) ) ;
#23811=DIRECTION ( 'NONE',  ( -0.000000000000000000, -0.000000000000000000, -1.000000000000000000 ) ) ;
#23812=ADVANCED_FACE ( 'NONE', ( #7934 ), #9287, .F. ) ;
#23813=CARTESIAN_POINT ( 'NONE',  ( -34.00000000000000000, -3.851859888774471706E-31, 10.49999999999999822 ) ) ;
#23817=ORIENTED_EDGE ( 'NONE', *, *, #15769, .F. ) ;
#23821=DIRECTION ( 'NONE',  ( -0.000000000000000000, -0.000000000000000000, 1.000000000000000000 ) ) ;
#23833=ORIENTED_EDGE ( 'NONE', *, *, #4574, .T. ) ;
#23838=CONICAL_SURFACE ( 'NONE', #14469, 1.999999999999994449, 1.029744258676653201 ) ;
#23846=CARTESIAN_POINT ( 'NONE',  ( -42.00000000000000000, -26.82133436441678853, 0.000000000000000000 ) ) ;
#23857=CIRCLE ( 'NONE', #488, 11.00000000000000711 ) ;
#23881=VECTOR ( 'NONE', #10301, 1000.000000000000000 ) ;
#23894=ORIENTED_EDGE ( 'NONE', *, *, #13182, .F. ) ;
#23899=ORIENTED_EDGE ( 'NONE', *, *, #9092, .F. ) ;
#23901=ORIENTED_EDGE ( 'NONE', *, *, #16791, .F. ) ;
#23903=CARTESIAN_POINT ( 'NONE',  ( -19.84999999999999787, -16.67999999999984695, 14.50000000000000000 ) ) ;
#23906=DIRECTION ( 'NONE',  ( -0.000000000000000000, -0.000000000000000000, -1.000000000000000000 ) ) ;
#23908=VECTOR ( 'NONE', #21555, 1000.000000000000000 ) ;
#23917=DIRECTION ( 'NONE',  ( -0.000000000000000000, 1.000000000000000000, 0.000000000000000000 ) ) ;
#23922=VECTOR ( 'NONE', #22516, 1000.000000000000000 ) ;
#23939=DIRECTION ( 'NONE',  ( 0.000000000000000000, -1.000000000000000000, 0.000000000000000000 ) ) ;
#23951=DIRECTION ( 'NONE',  ( -0.000000000000000000, 1.000000000000000000, -0.000000000000000000 ) ) ;
#23955=DIRECTION ( 'NONE',  ( 1.000000000000000000, 0.000000000000000000, 0.000000000000000000 ) ) ;
#23965=AXIS2_PLACEMENT_3D ( 'NONE', #4714, #4478, #17139 ) ;
#23966=ORIENTED_EDGE ( 'NONE', *, *, #21860, .T. ) ;
#23972=ADVANCED_FACE ( 'NONE', ( #6617 ), #10260, .T. ) ;
#23977=CARTESIAN_POINT ( 'NONE',  ( -31.10231664966676846, -45.36128193761570770, 12.00000000000000000 ) ) ;
#23979=CIRCLE ( 'NONE', #1773, 2.024999999999999911 ) ;
#23988=DIRECTION ( 'NONE',  ( 0.8757121056631642642, -0.4828336235133043886, 0.000000000000000000 ) ) ;
#23989=VERTEX_POINT ( 'NONE', #12562 ) ;
#23996=LINE ( 'NONE', #14713, #9106 ) ;
#24000=FACE_OUTER_BOUND ( 'NONE', #9431, .T. ) ;
#24006=DIRECTION ( 'NONE',  ( 0.000000000000000000, -0.000000000000000000, 1.000000000000000000 ) ) ;
#24007=CARTESIAN_POINT ( 'NONE',  ( 40.29291594121673370, -26.62062637246459573, 11.00000000000000000 ) ) ;
#24017=ORIENTED_EDGE ( 'NONE', *, *, #19394, .F. ) ;
#24022=CIRCLE ( 'NONE', #17795, 1.999999999999994449 ) ;
#24028=ADVANCED_FACE ( 'NONE', ( #10850 ), #22117, .F. ) ;
#24030=ORIENTED_EDGE ( 'NONE', *, *, #6346, .T. ) ;
#24032=EDGE_CURVE ( 'NONE', #21975, #14074, #23585, .T. ) ;
#24037=VECTOR ( 'NONE', #8409, 1000.000000000000000 ) ;
#24040=CARTESIAN_POINT ( 'NONE',  ( 21.13207267780287069, 38.32709852940855910, 12.00000000000000000 ) ) ;
#24045=VERTEX_POINT ( 'NONE', #8910 ) ;
#24047=AXIS2_PLACEMENT_3D ( 'NONE', #15328, #461, #23939 ) ;
#24048=LINE ( 'NONE', #12923, #10667 ) ;
#24064=DIRECTION ( 'NONE',  ( -1.000000000000000000, 0.000000000000000000, 0.000000000000000000 ) ) ;
#24068=ORIENTED_EDGE ( 'NONE', *, *, #12853, .T. ) ;
#24069=ORIENTED_EDGE ( 'NONE', *, *, #4791, .F. ) ;
#24081=EDGE_LOOP ( 'NONE', ( #876, #22549, #6620, #23901 ) ) ;
#24084=FACE_OUTER_BOUND ( 'NONE', #14368, .T. ) ;
#24090=CARTESIAN_POINT ( 'NONE',  ( 42.00000000000000000, -26.82133436441678853, 11.00000000000000000 ) ) ;
#24091=DIRECTION ( 'NONE',  ( 0.000000000000000000, 0.000000000000000000, -1.000000000000000000 ) ) ;
#24093=ORIENTED_EDGE ( 'NONE', *, *, #3438, .T. ) ;
#24097=EDGE_CURVE ( 'NONE', #19436, #671, #18086, .T. ) ;
#24142=COLOUR_RGB('Sky Blue',0.24,0.69,0.87);
#24143=FILL_AREA_STYLE_COLOUR('',#24142);
#24144=FILL_AREA_STYLE('',(#24143));
#24145=SURFACE_STYLE_FILL_AREA(#24144);
#24146=SURFACE_SIDE_STYLE('',(#24145));
#24147=SURFACE_STYLE_USAGE(.BOTH.,#24146);
#24148=PRESENTATION_STYLE_ASSIGNMENT((#24147));
ENDSEC;
END-ISO-10303-21;
